ISO-10303-21;
HEADER;
/* Generated by software containing ST-Developer
 * from STEP Tools, Inc. (www.steptools.com) 
 */

FILE_DESCRIPTION(
/* description */ (''),
/* implementation_level */ '2;1');

FILE_NAME(
/* name */ 'Hex nut M3.step',
/* time_stamp */ '2026-11-12T00:53:40-08:00',
/* author */ (''),
/* organization */ (''),
/* preprocessor_version */ 'ST-DEVELOPER v20.2',
/* originating_system */ 'Autodesk Translation Framework v15.17.0.0',
/* authorisation */ '');

FILE_SCHEMA (('AUTOMOTIVE_DESIGN { 1 0 10303 214 3 1 1 }'));
ENDSEC;

DATA;
#10=MECHANICAL_DESIGN_GEOMETRIC_PRESENTATION_REPRESENTATION('',(#578),#22129);
#158=B_SPLINE_SURFACE_WITH_KNOTS('',3,3,((#20915,#20916,#20917,#20918,#20919,
#20920,#20921,#20922,#20923,#20924,#20925,#20926,#20927,#20928,#20929,#20930,
#20931,#20932,#20933,#20934,#20935,#20936,#20937,#20938,#20939,#20940,#20941,
#20942,#20943,#20944,#20945,#20946,#20947,#20948,#20949,#20950),(#20951,
#20952,#20953,#20954,#20955,#20956,#20957,#20958,#20959,#20960,#20961,#20962,
#20963,#20964,#20965,#20966,#20967,#20968,#20969,#20970,#20971,#20972,#20973,
#20974,#20975,#20976,#20977,#20978,#20979,#20980,#20981,#20982,#20983,#20984,
#20985,#20986),(#20987,#20988,#20989,#20990,#20991,#20992,#20993,#20994,
#20995,#20996,#20997,#20998,#20999,#21000,#21001,#21002,#21003,#21004,#21005,
#21006,#21007,#21008,#21009,#21010,#21011,#21012,#21013,#21014,#21015,#21016,
#21017,#21018,#21019,#21020,#21021,#21022),(#21023,#21024,#21025,#21026,
#21027,#21028,#21029,#21030,#21031,#21032,#21033,#21034,#21035,#21036,#21037,
#21038,#21039,#21040,#21041,#21042,#21043,#21044,#21045,#21046,#21047,#21048,
#21049,#21050,#21051,#21052,#21053,#21054,#21055,#21056,#21057,#21058)),
 .UNSPECIFIED.,.F.,.F.,.F.,(4,4),(4,1,1,1,1,1,1,1,1,1,1,1,1,1,1,1,1,1,1,
1,1,1,1,1,1,1,1,1,1,1,1,1,1,4),(0.,0.0321584099938622),(11.8553612635794,
12.830508595889,13.8056559281987,14.7808032605084,15.755950592818,16.7310979251277,
17.7062452574374,18.681392589747,19.6565399220567,20.6316872543664,21.606834586676,
22.5819819189857,23.5571292512954,24.532276583605,25.5074239159147,26.4825712482243,
27.457718580534,28.4328659128437,29.4080132451533,30.383160577463,31.3583079097727,
32.3334552420823,33.308602574392,34.2837499067017,35.2588972390113,36.234044571321,
37.2091919036307,38.1843392359403,39.15948656825,40.1346339005596,41.1097812328693,
42.084928565179,43.0600758974886,44.0352232297983),.UNSPECIFIED.);
#159=B_SPLINE_SURFACE_WITH_KNOTS('',3,3,((#21182,#21183,#21184,#21185,#21186,
#21187,#21188,#21189,#21190,#21191,#21192,#21193,#21194,#21195,#21196,#21197,
#21198,#21199,#21200,#21201,#21202,#21203,#21204,#21205,#21206,#21207,#21208,
#21209,#21210,#21211,#21212,#21213,#21214,#21215,#21216,#21217),(#21218,
#21219,#21220,#21221,#21222,#21223,#21224,#21225,#21226,#21227,#21228,#21229,
#21230,#21231,#21232,#21233,#21234,#21235,#21236,#21237,#21238,#21239,#21240,
#21241,#21242,#21243,#21244,#21245,#21246,#21247,#21248,#21249,#21250,#21251,
#21252,#21253),(#21254,#21255,#21256,#21257,#21258,#21259,#21260,#21261,
#21262,#21263,#21264,#21265,#21266,#21267,#21268,#21269,#21270,#21271,#21272,
#21273,#21274,#21275,#21276,#21277,#21278,#21279,#21280,#21281,#21282,#21283,
#21284,#21285,#21286,#21287,#21288,#21289),(#21290,#21291,#21292,#21293,
#21294,#21295,#21296,#21297,#21298,#21299,#21300,#21301,#21302,#21303,#21304,
#21305,#21306,#21307,#21308,#21309,#21310,#21311,#21312,#21313,#21314,#21315,
#21316,#21317,#21318,#21319,#21320,#21321,#21322,#21323,#21324,#21325)),
 .UNSPECIFIED.,.F.,.F.,.F.,(4,4),(4,1,1,1,1,1,1,1,1,1,1,1,1,1,1,1,1,1,1,
1,1,1,1,1,1,1,1,1,1,1,1,1,1,4),(0.,0.0321584099938622),(14.3984001269719,
15.3735474592815,16.3486947915912,17.3238421239009,18.2989894562105,19.2741367885202,
20.2492841208299,21.2244314531395,22.1995787854492,23.1747261177589,24.1498734500685,
25.1250207823782,26.1001681146879,27.0753154469975,28.0504627793072,29.0256101116168,
30.0007574439265,30.9759047762362,31.9510521085458,32.9261994408555,33.9013467731652,
34.8764941054748,35.8516414377845,36.8267887700942,37.8019361024038,38.7770834347135,
39.7522307670232,40.7273780993328,41.7025254316425,42.6776727639522,43.6528200962618,
44.6279674285715,45.6031147608811,46.5782620931908),.UNSPECIFIED.);
#501=B_SPLINE_CURVE_WITH_KNOTS('',3,(#20585,#20586,#20587,#20588,#20589,
#20590,#20591),.UNSPECIFIED.,.F.,.F.,(4,3,4),(-30.159289474462,-29.2544199692899,
-28.9853432330879),.UNSPECIFIED.);
#502=B_SPLINE_CURVE_WITH_KNOTS('',3,(#20597,#20598,#20599,#20600,#20601,
#20602,#20603,#20604,#20605,#20606,#20607,#20608,#20609,#20610,#20611,#20612,
#20613,#20614,#20615),.UNSPECIFIED.,.F.,.F.,(4,3,3,3,3,3,4),(26.4423043696954,
27.3041253046706,28.2792726369803,29.25441996929,30.2295673015996,31.2047146339093,
32.179861966219),.UNSPECIFIED.);
#503=B_SPLINE_CURVE_WITH_KNOTS('',3,(#20617,#20618,#20619,#20620,#20621,
#20622,#20623,#20624,#20625,#20626,#20627,#20628,#20629,#20630,#20631,#20632,
#20633,#20634,#20635,#20636,#20637,#20638),.UNSPECIFIED.,.F.,.F.,(4,3,3,
3,3,3,3,4),(-28.9853432330879,-28.2792726369803,-27.3041253046706,-26.3289779723609,
-25.3538306400513,-24.3786833077416,-23.403535975432,-22.7021579259084),
 .UNSPECIFIED.);
#504=B_SPLINE_CURVE_WITH_KNOTS('',3,(#20643,#20644,#20645,#20646,#20647,
#20648,#20649,#20650,#20651,#20652,#20653,#20654,#20655,#20656,#20657,#20658,
#20659,#20660,#20661,#20662,#20663,#20664,#20665,#20666,#20667),
 .UNSPECIFIED.,.F.,.F.,(4,3,3,3,3,3,3,3,4),(20.1591190625159,20.478093978503,
21.4532413108126,22.4283886431223,23.403535975432,24.3786833077416,25.3538306400513,
26.328977972361,26.4423043696954),.UNSPECIFIED.);
#505=B_SPLINE_CURVE_WITH_KNOTS('',3,(#20668,#20669,#20670,#20671,#20672,
#20673,#20674,#20675,#20676,#20677,#20678,#20679,#20680,#20681,#20682,#20683,
#20684,#20685,#20686,#20687,#20688,#20689,#20690,#20691,#20692),
 .UNSPECIFIED.,.F.,.F.,(4,3,3,3,3,3,3,3,4),(-22.7021579259084,-22.4283886431223,
-21.4532413108126,-20.478093978503,-19.5029466461933,-18.5277993138836,
-17.552651981574,-16.5775046492643,-16.4189726187288),.UNSPECIFIED.);
#506=B_SPLINE_CURVE_WITH_KNOTS('',3,(#20697,#20698,#20699,#20700,#20701,
#20702,#20703,#20704,#20705,#20706,#20707,#20708,#20709,#20710,#20711,#20712,
#20713,#20714,#20715,#20716,#20717,#20718),.UNSPECIFIED.,.F.,.F.,(4,3,3,
3,3,3,3,4),(13.8759337553363,14.627209984645,15.6023573169546,16.5775046492643,
17.552651981574,18.5277993138836,19.5029466461933,20.1591190625159),
 .UNSPECIFIED.);
#507=B_SPLINE_CURVE_WITH_KNOTS('',3,(#20719,#20720,#20721,#20722,#20723,
#20724,#20725,#20726,#20727,#20728,#20729,#20730,#20731,#20732,#20733,#20734,
#20735,#20736,#20737,#20738,#20739,#20740),.UNSPECIFIED.,.F.,.F.,(4,3,3,
3,3,3,3,4),(-16.4189726187288,-15.6023573169546,-14.627209984645,-13.6520626523353,
-12.6769153200256,-11.701767987716,-10.7266206554063,-10.1357873115492),
 .UNSPECIFIED.);
#508=B_SPLINE_CURVE_WITH_KNOTS('',3,(#20746,#20747,#20748,#20749,#20750,
#20751,#20752,#20753,#20754,#20755,#20756,#20757,#20758),.UNSPECIFIED.,
 .F.,.F.,(4,3,3,3,4),(-3.8526020043696,-2.92544199692899,-1.95029466461933,
-0.975147332309664,0.),.UNSPECIFIED.);
#509=B_SPLINE_CURVE_WITH_KNOTS('',3,(#20761,#20762,#20763,#20764,#20765,
#20766,#20767,#20768,#20769,#20770,#20771,#20772,#20773,#20774,#20775,#20776,
#20777,#20778,#20779),.UNSPECIFIED.,.F.,.F.,(4,3,3,3,3,3,4),(2.02057249175693,
2.925441996929,3.90058932923866,4.87573666154832,5.85088399385799,6.82603132616766,
7.59274844815668),.UNSPECIFIED.);
#510=B_SPLINE_CURVE_WITH_KNOTS('',3,(#20785,#20786,#20787,#20788,#20789,
#20790,#20791),.UNSPECIFIED.,.F.,.F.,(4,1,1,1,4),(40.8407044966673,41.1097812328693,
42.084928565179,43.0600758974886,44.0352232297983),.UNSPECIFIED.);
#511=B_SPLINE_CURVE_WITH_KNOTS('',3,(#20794,#20795,#20796,#20797,#20798,
#20799,#20800),.UNSPECIFIED.,.F.,.F.,(4,1,1,1,4),(40.8407044966673,41.7025254316425,
42.6776727639522,43.6528200962618,44.5576896014339),.UNSPECIFIED.);
#512=B_SPLINE_CURVE_WITH_KNOTS('',3,(#20805,#20806,#20807,#20808,#20809,
#20810,#20811,#20812,#20813,#20814),.UNSPECIFIED.,.F.,.F.,(4,1,1,1,1,1,
1,4),(34.5575191894877,35.2588972390113,36.234044571321,37.2091919036307,
38.1843392359403,39.15948656825,40.1346339005596,40.8407044966673),
 .UNSPECIFIED.);
#513=B_SPLINE_CURVE_WITH_KNOTS('',3,(#20815,#20816,#20817,#20818,#20819,
#20820,#20821,#20822,#20823,#20824,#20825),.UNSPECIFIED.,.F.,.F.,(4,1,1,
1,1,1,1,1,4),(34.5575191894877,34.8764941054748,35.8516414377845,36.8267887700942,
37.8019361024038,38.7770834347135,39.7522307670232,40.7273780993328,40.8407044966673),
 .UNSPECIFIED.);
#514=B_SPLINE_CURVE_WITH_KNOTS('',3,(#20830,#20831,#20832,#20833,#20834,
#20835,#20836,#20837,#20838,#20839,#20840),.UNSPECIFIED.,.F.,.F.,(4,1,1,
1,1,1,1,1,4),(28.2743338823081,28.4328659128437,29.4080132451533,30.383160577463,
31.3583079097727,32.3334552420823,33.308602574392,34.2837499067017,34.5575191894877),
 .UNSPECIFIED.);
#515=B_SPLINE_CURVE_WITH_KNOTS('',3,(#20841,#20842,#20843,#20844,#20845,
#20846,#20847,#20848,#20849,#20850),.UNSPECIFIED.,.F.,.F.,(4,1,1,1,1,1,
1,4),(28.2743338823081,29.0256101116168,30.0007574439265,30.9759047762362,
31.9510521085458,32.9261994408555,33.9013467731652,34.5575191894877),
 .UNSPECIFIED.);
#516=B_SPLINE_CURVE_WITH_KNOTS('',3,(#20855,#20856,#20857,#20858,#20859,
#20860,#20861,#20862,#20863,#20864),.UNSPECIFIED.,.F.,.F.,(4,1,1,1,1,1,
1,4),(21.9911485751285,22.5819819189857,23.5571292512954,24.532276583605,
25.5074239159147,26.4825712482243,27.457718580534,28.2743338823081),
 .UNSPECIFIED.);
#517=B_SPLINE_CURVE_WITH_KNOTS('',3,(#20865,#20866,#20867,#20868,#20869,
#20870,#20871,#20872,#20873,#20874,#20875),.UNSPECIFIED.,.F.,.F.,(4,1,1,
1,1,1,1,1,4),(21.9911485751285,22.1995787854492,23.1747261177589,24.1498734500685,
25.1250207823782,26.1001681146879,27.0753154469975,28.0504627793072,28.2743338823081),
 .UNSPECIFIED.);
#518=B_SPLINE_CURVE_WITH_KNOTS('',3,(#20881,#20882,#20883,#20884,#20885),
 .UNSPECIFIED.,.F.,.F.,(4,1,4),(14.3984001269719,15.3735474592815,15.7079632679489),
 .UNSPECIFIED.);
#519=B_SPLINE_CURVE_WITH_KNOTS('',3,(#20888,#20889,#20890,#20891,#20892),
 .UNSPECIFIED.,.F.,.F.,(4,1,4),(13.8759337553363,14.7808032605084,15.7079632679489),
 .UNSPECIFIED.);
#520=B_SPLINE_CURVE_WITH_KNOTS('',3,(#20894,#20895,#20896,#20897,#20898,
#20899,#20900,#20901,#20902,#20903,#20904),.UNSPECIFIED.,.F.,.F.,(4,1,1,
1,1,1,1,1,4),(15.7079632679489,15.755950592818,16.7310979251277,17.7062452574374,
18.681392589747,19.6565399220567,20.6316872543664,21.606834586676,21.9911485751285),
 .UNSPECIFIED.);
#521=B_SPLINE_CURVE_WITH_KNOTS('',3,(#20905,#20906,#20907,#20908,#20909,
#20910,#20911,#20912,#20913,#20914),.UNSPECIFIED.,.F.,.F.,(4,1,1,1,1,1,
1,4),(15.7079632679489,16.3486947915912,17.3238421239009,18.2989894562105,
19.2741367885202,20.2492841208299,21.2244314531395,21.9911485751285),
 .UNSPECIFIED.);
#522=B_SPLINE_CURVE_WITH_KNOTS('',3,(#21059,#21060,#21061,#21062,#21063,
#21064,#21065,#21066,#21067,#21068,#21069,#21070,#21071,#21072,#21073,#21074,
#21075,#21076,#21077,#21078,#21079,#21080,#21081,#21082,#21083,#21084,#21085,
#21086,#21087,#21088,#21089,#21090,#21091,#21092,#21093,#21094,#21095,#21096,
#21097,#21098,#21099,#21100,#21101,#21102,#21103,#21104,#21105,#21106,#21107),
 .UNSPECIFIED.,.F.,.F.,(4,3,3,3,3,3,3,3,3,3,3,3,3,3,3,3,4),(0.,0.0320333804888866,
0.0505515708593653,0.0603413132804416,0.0917900141854983,0.108096115778005,
0.122914675479851,0.145143248337739,0.168151513577436,0.177516949333476,
0.202471322707608,0.21794283081622,0.231200110368267,0.247503117401854,
0.263651632124391,0.277334442830003,0.286347380332244),.UNSPECIFIED.);
#523=B_SPLINE_CURVE_WITH_KNOTS('',3,(#21108,#21109,#21110,#21111,#21112,
#21113,#21114,#21115,#21116,#21117,#21118,#21119,#21120,#21121,#21122,#21123,
#21124,#21125,#21126,#21127,#21128,#21129,#21130,#21131,#21132,#21133,#21134,
#21135,#21136,#21137,#21138,#21139,#21140,#21141,#21142,#21143,#21144,#21145,
#21146,#21147,#21148,#21149,#21150,#21151,#21152,#21153,#21154,#21155,#21156),
 .UNSPECIFIED.,.F.,.F.,(4,3,3,3,3,3,3,3,3,3,3,3,3,3,3,3,4),(0.,0.0274305464075637,
0.0492901149097146,0.0591933555873536,0.0887250095166089,0.100015570674795,
0.108381796308415,0.130826479038955,0.152531076563578,0.162815893631175,
0.190691958353668,0.212372986031639,0.222945305605857,0.245534254906135,
0.257847836118801,0.274320152521146,0.28514280399515),.UNSPECIFIED.);
#524=B_SPLINE_CURVE_WITH_KNOTS('',3,(#21157,#21158,#21159,#21160,#21161,
#21162,#21163,#21164,#21165,#21166,#21167,#21168,#21169,#21170,#21171,#21172,
#21173,#21174,#21175,#21176,#21177,#21178,#21179,#21180,#21181),
 .UNSPECIFIED.,.F.,.F.,(4,3,3,3,3,3,3,3,4),(-10.1357873115492,-9.75147332309665,
-8.77632599078699,-7.80117865847732,-6.82603132616766,-5.85088399385799,
-4.87573666154833,-3.90058932923866,-3.8526020043696),.UNSPECIFIED.);
#525=B_SPLINE_CURVE_WITH_KNOTS('',3,(#21326,#21327,#21328,#21329,#21330,
#21331,#21332,#21333,#21334,#21335,#21336,#21337,#21338,#21339,#21340,#21341,
#21342,#21343,#21344,#21345,#21346,#21347,#21348,#21349,#21350,#21351,#21352,
#21353,#21354,#21355,#21356,#21357,#21358,#21359,#21360,#21361,#21362,#21363,
#21364,#21365,#21366,#21367,#21368,#21369,#21370,#21371,#21372,#21373,#21374),
 .UNSPECIFIED.,.F.,.F.,(4,3,3,3,3,3,3,3,3,3,3,3,3,3,3,3,4),(0.,0.0274305890506951,
0.0492901290331875,0.0591933603491513,0.0887250177779717,0.100015607166709,
0.108381835831352,0.13082647903896,0.152531071764912,0.162815892251191,
0.190691957318683,0.212372984486691,0.22294529735758,0.245534140364172,
0.257847701250626,0.274320152521159,0.285142803995162),.UNSPECIFIED.);
#526=B_SPLINE_CURVE_WITH_KNOTS('',3,(#21375,#21376,#21377,#21378,#21379,
#21380,#21381,#21382,#21383,#21384,#21385,#21386,#21387,#21388,#21389,#21390,
#21391,#21392,#21393,#21394,#21395,#21396,#21397,#21398,#21399),
 .UNSPECIFIED.,.F.,.F.,(4,3,3,3,3,3,3,3,4),(7.59274844815668,7.80117865847732,
8.77632599078698,9.75147332309665,10.7266206554063,11.701767987716,12.6769153200256,
13.6520626523353,13.8759337553363),.UNSPECIFIED.);
#527=B_SPLINE_CURVE_WITH_KNOTS('',3,(#21400,#21401,#21402,#21403,#21404,
#21405,#21406,#21407,#21408,#21409,#21410,#21411,#21412,#21413,#21414,#21415,
#21416,#21417,#21418,#21419,#21420,#21421,#21422,#21423,#21424,#21425,#21426,
#21427,#21428,#21429,#21430,#21431,#21432,#21433,#21434,#21435,#21436,#21437,
#21438,#21439,#21440,#21441,#21442,#21443,#21444,#21445,#21446,#21447,#21448),
 .UNSPECIFIED.,.F.,.F.,(4,3,3,3,3,3,3,3,3,3,3,3,3,3,3,3,4),(0.,0.0320334058164849,
0.0505515938322513,0.0603413311462071,0.0917900214840119,0.108096111687201,
0.122914678304232,0.145143248337743,0.168151527562726,0.177516955081398,
0.202471327018552,0.217942288122009,0.231200024743484,0.24750284136614,
0.263651600306541,0.277334442830014,0.286347380332252),.UNSPECIFIED.);
#560=SHAPE_REPRESENTATION_RELATIONSHIP('SRR','None',#22180,#569);
#569=ADVANCED_BREP_SHAPE_REPRESENTATION('',(#587),#22126);
#578=STYLED_ITEM('',(#22236),#587);
#587=MANIFOLD_SOLID_BREP('Body1',#8809);
#635=FACE_BOUND('',#1866,.T.);
#636=FACE_BOUND('',#1875,.T.);
#881=PLANE('',#9413);
#882=PLANE('',#9415);
#883=PLANE('',#9416);
#884=PLANE('',#9417);
#885=PLANE('',#9418);
#886=PLANE('',#9419);
#887=PLANE('',#9420);
#888=PLANE('',#9421);
#1324=FACE_OUTER_BOUND('',#1852,.T.);
#1325=FACE_OUTER_BOUND('',#1853,.T.);
#1326=FACE_OUTER_BOUND('',#1854,.T.);
#1327=FACE_OUTER_BOUND('',#1855,.T.);
#1328=FACE_OUTER_BOUND('',#1856,.T.);
#1329=FACE_OUTER_BOUND('',#1857,.T.);
#1330=FACE_OUTER_BOUND('',#1858,.T.);
#1331=FACE_OUTER_BOUND('',#1859,.T.);
#1332=FACE_OUTER_BOUND('',#1860,.T.);
#1333=FACE_OUTER_BOUND('',#1861,.T.);
#1334=FACE_OUTER_BOUND('',#1862,.T.);
#1335=FACE_OUTER_BOUND('',#1863,.T.);
#1336=FACE_OUTER_BOUND('',#1864,.T.);
#1337=FACE_OUTER_BOUND('',#1865,.T.);
#1338=FACE_OUTER_BOUND('',#1867,.T.);
#1339=FACE_OUTER_BOUND('',#1868,.T.);
#1340=FACE_OUTER_BOUND('',#1869,.T.);
#1341=FACE_OUTER_BOUND('',#1870,.T.);
#1342=FACE_OUTER_BOUND('',#1871,.T.);
#1343=FACE_OUTER_BOUND('',#1872,.T.);
#1344=FACE_OUTER_BOUND('',#1873,.T.);
#1345=FACE_OUTER_BOUND('',#1874,.T.);
#1852=EDGE_LOOP('',(#7914,#7915,#7916));
#1853=EDGE_LOOP('',(#7917,#7918,#7919,#7920,#7921));
#1854=EDGE_LOOP('',(#7922,#7923,#7924,#7925));
#1855=EDGE_LOOP('',(#7926,#7927,#7928,#7929));
#1856=EDGE_LOOP('',(#7930,#7931,#7932,#7933));
#1857=EDGE_LOOP('',(#7934,#7935,#7936,#7937));
#1858=EDGE_LOOP('',(#7938,#7939,#7940,#7941));
#1859=EDGE_LOOP('',(#7942,#7943,#7944,#7945));
#1860=EDGE_LOOP('',(#7946,#7947,#7948,#7949));
#1861=EDGE_LOOP('',(#7950,#7951,#7952,#7953));
#1862=EDGE_LOOP('',(#7954,#7955,#7956,#7957));
#1863=EDGE_LOOP('',(#7958,#7959,#7960,#7961,#7962,#7963,#7964,#7965,#7966,
#7967,#7968,#7969,#7970,#7971));
#1864=EDGE_LOOP('',(#7972,#7973,#7974,#7975,#7976,#7977,#7978,#7979,#7980,
#7981,#7982,#7983,#7984));
#1865=EDGE_LOOP('',(#7985,#7986,#7987,#7988,#7989,#7990));
#1866=EDGE_LOOP('',(#7991,#7992,#7993,#7994));
#1867=EDGE_LOOP('',(#7995,#7996,#7997,#7998));
#1868=EDGE_LOOP('',(#7999,#8000,#8001,#8002));
#1869=EDGE_LOOP('',(#8003,#8004,#8005,#8006));
#1870=EDGE_LOOP('',(#8007,#8008,#8009,#8010));
#1871=EDGE_LOOP('',(#8011,#8012,#8013,#8014));
#1872=EDGE_LOOP('',(#8015,#8016,#8017,#8018));
#1873=EDGE_LOOP('',(#8019,#8020,#8021,#8022));
#1874=EDGE_LOOP('',(#8023,#8024,#8025,#8026,#8027,#8028));
#1875=EDGE_LOOP('',(#8029,#8030,#8031,#8032,#8033));
#2614=LINE('',#20582,#3344);
#2615=LINE('',#20595,#3345);
#2616=LINE('',#20642,#3346);
#2617=LINE('',#20696,#3347);
#2618=LINE('',#20744,#3348);
#2619=LINE('',#20783,#3349);
#2620=LINE('',#20804,#3350);
#2621=LINE('',#20829,#3351);
#2622=LINE('',#20854,#3352);
#2623=LINE('',#20879,#3353);
#2624=LINE('',#21452,#3354);
#2625=LINE('',#21454,#3355);
#2626=LINE('',#21456,#3356);
#2627=LINE('',#21458,#3357);
#2628=LINE('',#21460,#3358);
#2629=LINE('',#21461,#3359);
#2630=LINE('',#21466,#3360);
#2631=LINE('',#21467,#3361);
#2632=LINE('',#21468,#3362);
#2633=LINE('',#21471,#3363);
#2634=LINE('',#21472,#3364);
#2635=LINE('',#21475,#3365);
#2636=LINE('',#21476,#3366);
#2637=LINE('',#21479,#3367);
#2638=LINE('',#21480,#3368);
#2639=LINE('',#21483,#3369);
#2640=LINE('',#21484,#3370);
#2641=LINE('',#21486,#3371);
#3344=VECTOR('',#11156,0.15);
#3345=VECTOR('',#11161,0.15);
#3346=VECTOR('',#11166,0.15);
#3347=VECTOR('',#11169,0.15);
#3348=VECTOR('',#11172,0.15);
#3349=VECTOR('',#11177,0.1543);
#3350=VECTOR('',#11182,0.1543);
#3351=VECTOR('',#11185,0.1543);
#3352=VECTOR('',#11188,0.1543);
#3353=VECTOR('',#11191,0.1543);
#3354=VECTOR('',#11198,1.);
#3355=VECTOR('',#11199,1.);
#3356=VECTOR('',#11200,1.);
#3357=VECTOR('',#11201,1.);
#3358=VECTOR('',#11202,1.);
#3359=VECTOR('',#11203,1.);
#3360=VECTOR('',#11208,1.);
#3361=VECTOR('',#11209,1.);
#3362=VECTOR('',#11210,1.);
#3363=VECTOR('',#11213,1.);
#3364=VECTOR('',#11214,1.);
#3365=VECTOR('',#11217,1.);
#3366=VECTOR('',#11218,1.);
#3367=VECTOR('',#11221,1.);
#3368=VECTOR('',#11222,1.);
#3369=VECTOR('',#11225,1.);
#3370=VECTOR('',#11226,1.);
#3371=VECTOR('',#11229,1.);
#3511=CIRCLE('',#9398,0.12645);
#3512=CIRCLE('',#9400,0.12645);
#3513=CIRCLE('',#9404,0.12645);
#3514=CIRCLE('',#9406,0.1543);
#3515=CIRCLE('',#9411,0.1543);
#4288=VERTEX_POINT('',#20580);
#4289=VERTEX_POINT('',#20581);
#4290=VERTEX_POINT('',#20583);
#4291=VERTEX_POINT('',#20593);
#4292=VERTEX_POINT('',#20594);
#4293=VERTEX_POINT('',#20596);
#4294=VERTEX_POINT('',#20640);
#4295=VERTEX_POINT('',#20641);
#4296=VERTEX_POINT('',#20694);
#4297=VERTEX_POINT('',#20695);
#4298=VERTEX_POINT('',#20742);
#4299=VERTEX_POINT('',#20743);
#4300=VERTEX_POINT('',#20745);
#4301=VERTEX_POINT('',#20759);
#4302=VERTEX_POINT('',#20781);
#4303=VERTEX_POINT('',#20782);
#4304=VERTEX_POINT('',#20784);
#4305=VERTEX_POINT('',#20792);
#4306=VERTEX_POINT('',#20802);
#4307=VERTEX_POINT('',#20803);
#4308=VERTEX_POINT('',#20827);
#4309=VERTEX_POINT('',#20828);
#4310=VERTEX_POINT('',#20852);
#4311=VERTEX_POINT('',#20853);
#4312=VERTEX_POINT('',#20877);
#4313=VERTEX_POINT('',#20878);
#4314=VERTEX_POINT('',#20880);
#4315=VERTEX_POINT('',#20886);
#4316=VERTEX_POINT('',#21450);
#4317=VERTEX_POINT('',#21451);
#4318=VERTEX_POINT('',#21453);
#4319=VERTEX_POINT('',#21455);
#4320=VERTEX_POINT('',#21457);
#4321=VERTEX_POINT('',#21459);
#4322=VERTEX_POINT('',#21464);
#4323=VERTEX_POINT('',#21465);
#4324=VERTEX_POINT('',#21470);
#4325=VERTEX_POINT('',#21474);
#4326=VERTEX_POINT('',#21478);
#4327=VERTEX_POINT('',#21482);
#5510=EDGE_CURVE('',#4288,#4289,#2614,.T.);
#5511=EDGE_CURVE('',#4290,#4289,#3511,.F.);
#5512=EDGE_CURVE('',#4290,#4288,#501,.T.);
#5513=EDGE_CURVE('',#4291,#4292,#2615,.T.);
#5514=EDGE_CURVE('',#4292,#4293,#502,.T.);
#5515=EDGE_CURVE('',#4289,#4293,#3512,.F.);
#5516=EDGE_CURVE('',#4288,#4291,#503,.T.);
#5517=EDGE_CURVE('',#4294,#4295,#2616,.T.);
#5518=EDGE_CURVE('',#4295,#4292,#504,.T.);
#5519=EDGE_CURVE('',#4291,#4294,#505,.T.);
#5520=EDGE_CURVE('',#4296,#4297,#2617,.T.);
#5521=EDGE_CURVE('',#4297,#4295,#506,.T.);
#5522=EDGE_CURVE('',#4294,#4296,#507,.T.);
#5523=EDGE_CURVE('',#4298,#4299,#2618,.T.);
#5524=EDGE_CURVE('',#4298,#4300,#508,.T.);
#5525=EDGE_CURVE('',#4301,#4300,#3513,.T.);
#5526=EDGE_CURVE('',#4301,#4299,#509,.T.);
#5527=EDGE_CURVE('',#4302,#4303,#2619,.T.);
#5528=EDGE_CURVE('',#4303,#4304,#510,.T.);
#5529=EDGE_CURVE('',#4305,#4304,#3514,.T.);
#5530=EDGE_CURVE('',#4302,#4305,#511,.T.);
#5531=EDGE_CURVE('',#4306,#4307,#2620,.T.);
#5532=EDGE_CURVE('',#4307,#4303,#512,.T.);
#5533=EDGE_CURVE('',#4306,#4302,#513,.T.);
#5534=EDGE_CURVE('',#4308,#4309,#2621,.T.);
#5535=EDGE_CURVE('',#4309,#4307,#514,.T.);
#5536=EDGE_CURVE('',#4308,#4306,#515,.T.);
#5537=EDGE_CURVE('',#4310,#4311,#2622,.T.);
#5538=EDGE_CURVE('',#4311,#4309,#516,.T.);
#5539=EDGE_CURVE('',#4310,#4308,#517,.T.);
#5540=EDGE_CURVE('',#4312,#4313,#2623,.T.);
#5541=EDGE_CURVE('',#4314,#4312,#518,.T.);
#5542=EDGE_CURVE('',#4315,#4314,#3515,.T.);
#5543=EDGE_CURVE('',#4315,#4313,#519,.T.);
#5544=EDGE_CURVE('',#4313,#4311,#520,.T.);
#5545=EDGE_CURVE('',#4312,#4310,#521,.T.);
#5546=EDGE_CURVE('',#4304,#4290,#522,.T.);
#5547=EDGE_CURVE('',#4300,#4315,#523,.T.);
#5548=EDGE_CURVE('',#4296,#4298,#524,.T.);
#5549=EDGE_CURVE('',#4293,#4305,#525,.T.);
#5550=EDGE_CURVE('',#4299,#4297,#526,.T.);
#5551=EDGE_CURVE('',#4314,#4301,#527,.T.);
#5552=EDGE_CURVE('',#4316,#4317,#2624,.T.);
#5553=EDGE_CURVE('',#4317,#4318,#2625,.T.);
#5554=EDGE_CURVE('',#4318,#4319,#2626,.T.);
#5555=EDGE_CURVE('',#4319,#4320,#2627,.T.);
#5556=EDGE_CURVE('',#4320,#4321,#2628,.T.);
#5557=EDGE_CURVE('',#4321,#4316,#2629,.T.);
#5558=EDGE_CURVE('',#4322,#4323,#2630,.T.);
#5559=EDGE_CURVE('',#4323,#4316,#2631,.T.);
#5560=EDGE_CURVE('',#4322,#4321,#2632,.T.);
#5561=EDGE_CURVE('',#4324,#4322,#2633,.T.);
#5562=EDGE_CURVE('',#4324,#4320,#2634,.T.);
#5563=EDGE_CURVE('',#4325,#4324,#2635,.T.);
#5564=EDGE_CURVE('',#4325,#4319,#2636,.T.);
#5565=EDGE_CURVE('',#4326,#4325,#2637,.T.);
#5566=EDGE_CURVE('',#4326,#4318,#2638,.T.);
#5567=EDGE_CURVE('',#4327,#4326,#2639,.T.);
#5568=EDGE_CURVE('',#4327,#4317,#2640,.T.);
#5569=EDGE_CURVE('',#4323,#4327,#2641,.T.);
#7914=ORIENTED_EDGE('',*,*,#5510,.T.);
#7915=ORIENTED_EDGE('',*,*,#5511,.F.);
#7916=ORIENTED_EDGE('',*,*,#5512,.T.);
#7917=ORIENTED_EDGE('',*,*,#5513,.T.);
#7918=ORIENTED_EDGE('',*,*,#5514,.T.);
#7919=ORIENTED_EDGE('',*,*,#5515,.F.);
#7920=ORIENTED_EDGE('',*,*,#5510,.F.);
#7921=ORIENTED_EDGE('',*,*,#5516,.T.);
#7922=ORIENTED_EDGE('',*,*,#5517,.T.);
#7923=ORIENTED_EDGE('',*,*,#5518,.T.);
#7924=ORIENTED_EDGE('',*,*,#5513,.F.);
#7925=ORIENTED_EDGE('',*,*,#5519,.T.);
#7926=ORIENTED_EDGE('',*,*,#5520,.T.);
#7927=ORIENTED_EDGE('',*,*,#5521,.T.);
#7928=ORIENTED_EDGE('',*,*,#5517,.F.);
#7929=ORIENTED_EDGE('',*,*,#5522,.T.);
#7930=ORIENTED_EDGE('',*,*,#5523,.F.);
#7931=ORIENTED_EDGE('',*,*,#5524,.T.);
#7932=ORIENTED_EDGE('',*,*,#5525,.F.);
#7933=ORIENTED_EDGE('',*,*,#5526,.T.);
#7934=ORIENTED_EDGE('',*,*,#5527,.T.);
#7935=ORIENTED_EDGE('',*,*,#5528,.T.);
#7936=ORIENTED_EDGE('',*,*,#5529,.F.);
#7937=ORIENTED_EDGE('',*,*,#5530,.F.);
#7938=ORIENTED_EDGE('',*,*,#5531,.T.);
#7939=ORIENTED_EDGE('',*,*,#5532,.T.);
#7940=ORIENTED_EDGE('',*,*,#5527,.F.);
#7941=ORIENTED_EDGE('',*,*,#5533,.F.);
#7942=ORIENTED_EDGE('',*,*,#5534,.T.);
#7943=ORIENTED_EDGE('',*,*,#5535,.T.);
#7944=ORIENTED_EDGE('',*,*,#5531,.F.);
#7945=ORIENTED_EDGE('',*,*,#5536,.F.);
#7946=ORIENTED_EDGE('',*,*,#5537,.T.);
#7947=ORIENTED_EDGE('',*,*,#5538,.T.);
#7948=ORIENTED_EDGE('',*,*,#5534,.F.);
#7949=ORIENTED_EDGE('',*,*,#5539,.F.);
#7950=ORIENTED_EDGE('',*,*,#5540,.F.);
#7951=ORIENTED_EDGE('',*,*,#5541,.F.);
#7952=ORIENTED_EDGE('',*,*,#5542,.F.);
#7953=ORIENTED_EDGE('',*,*,#5543,.T.);
#7954=ORIENTED_EDGE('',*,*,#5540,.T.);
#7955=ORIENTED_EDGE('',*,*,#5544,.T.);
#7956=ORIENTED_EDGE('',*,*,#5537,.F.);
#7957=ORIENTED_EDGE('',*,*,#5545,.F.);
#7958=ORIENTED_EDGE('',*,*,#5546,.F.);
#7959=ORIENTED_EDGE('',*,*,#5528,.F.);
#7960=ORIENTED_EDGE('',*,*,#5532,.F.);
#7961=ORIENTED_EDGE('',*,*,#5535,.F.);
#7962=ORIENTED_EDGE('',*,*,#5538,.F.);
#7963=ORIENTED_EDGE('',*,*,#5544,.F.);
#7964=ORIENTED_EDGE('',*,*,#5543,.F.);
#7965=ORIENTED_EDGE('',*,*,#5547,.F.);
#7966=ORIENTED_EDGE('',*,*,#5524,.F.);
#7967=ORIENTED_EDGE('',*,*,#5548,.F.);
#7968=ORIENTED_EDGE('',*,*,#5522,.F.);
#7969=ORIENTED_EDGE('',*,*,#5519,.F.);
#7970=ORIENTED_EDGE('',*,*,#5516,.F.);
#7971=ORIENTED_EDGE('',*,*,#5512,.F.);
#7972=ORIENTED_EDGE('',*,*,#5549,.F.);
#7973=ORIENTED_EDGE('',*,*,#5514,.F.);
#7974=ORIENTED_EDGE('',*,*,#5518,.F.);
#7975=ORIENTED_EDGE('',*,*,#5521,.F.);
#7976=ORIENTED_EDGE('',*,*,#5550,.F.);
#7977=ORIENTED_EDGE('',*,*,#5526,.F.);
#7978=ORIENTED_EDGE('',*,*,#5551,.F.);
#7979=ORIENTED_EDGE('',*,*,#5541,.T.);
#7980=ORIENTED_EDGE('',*,*,#5545,.T.);
#7981=ORIENTED_EDGE('',*,*,#5539,.T.);
#7982=ORIENTED_EDGE('',*,*,#5536,.T.);
#7983=ORIENTED_EDGE('',*,*,#5533,.T.);
#7984=ORIENTED_EDGE('',*,*,#5530,.T.);
#7985=ORIENTED_EDGE('',*,*,#5552,.T.);
#7986=ORIENTED_EDGE('',*,*,#5553,.T.);
#7987=ORIENTED_EDGE('',*,*,#5554,.T.);
#7988=ORIENTED_EDGE('',*,*,#5555,.T.);
#7989=ORIENTED_EDGE('',*,*,#5556,.T.);
#7990=ORIENTED_EDGE('',*,*,#5557,.T.);
#7991=ORIENTED_EDGE('',*,*,#5547,.T.);
#7992=ORIENTED_EDGE('',*,*,#5542,.T.);
#7993=ORIENTED_EDGE('',*,*,#5551,.T.);
#7994=ORIENTED_EDGE('',*,*,#5525,.T.);
#7995=ORIENTED_EDGE('',*,*,#5523,.T.);
#7996=ORIENTED_EDGE('',*,*,#5550,.T.);
#7997=ORIENTED_EDGE('',*,*,#5520,.F.);
#7998=ORIENTED_EDGE('',*,*,#5548,.T.);
#7999=ORIENTED_EDGE('',*,*,#5558,.T.);
#8000=ORIENTED_EDGE('',*,*,#5559,.T.);
#8001=ORIENTED_EDGE('',*,*,#5557,.F.);
#8002=ORIENTED_EDGE('',*,*,#5560,.F.);
#8003=ORIENTED_EDGE('',*,*,#5561,.T.);
#8004=ORIENTED_EDGE('',*,*,#5560,.T.);
#8005=ORIENTED_EDGE('',*,*,#5556,.F.);
#8006=ORIENTED_EDGE('',*,*,#5562,.F.);
#8007=ORIENTED_EDGE('',*,*,#5563,.T.);
#8008=ORIENTED_EDGE('',*,*,#5562,.T.);
#8009=ORIENTED_EDGE('',*,*,#5555,.F.);
#8010=ORIENTED_EDGE('',*,*,#5564,.F.);
#8011=ORIENTED_EDGE('',*,*,#5565,.T.);
#8012=ORIENTED_EDGE('',*,*,#5564,.T.);
#8013=ORIENTED_EDGE('',*,*,#5554,.F.);
#8014=ORIENTED_EDGE('',*,*,#5566,.F.);
#8015=ORIENTED_EDGE('',*,*,#5567,.T.);
#8016=ORIENTED_EDGE('',*,*,#5566,.T.);
#8017=ORIENTED_EDGE('',*,*,#5553,.F.);
#8018=ORIENTED_EDGE('',*,*,#5568,.F.);
#8019=ORIENTED_EDGE('',*,*,#5569,.T.);
#8020=ORIENTED_EDGE('',*,*,#5568,.T.);
#8021=ORIENTED_EDGE('',*,*,#5552,.F.);
#8022=ORIENTED_EDGE('',*,*,#5559,.F.);
#8023=ORIENTED_EDGE('',*,*,#5569,.F.);
#8024=ORIENTED_EDGE('',*,*,#5558,.F.);
#8025=ORIENTED_EDGE('',*,*,#5561,.F.);
#8026=ORIENTED_EDGE('',*,*,#5563,.F.);
#8027=ORIENTED_EDGE('',*,*,#5565,.F.);
#8028=ORIENTED_EDGE('',*,*,#5567,.F.);
#8029=ORIENTED_EDGE('',*,*,#5546,.T.);
#8030=ORIENTED_EDGE('',*,*,#5511,.T.);
#8031=ORIENTED_EDGE('',*,*,#5515,.T.);
#8032=ORIENTED_EDGE('',*,*,#5549,.T.);
#8033=ORIENTED_EDGE('',*,*,#5529,.T.);
#8294=CYLINDRICAL_SURFACE('',#9397,0.12645);
#8295=CYLINDRICAL_SURFACE('',#9399,0.12645);
#8296=CYLINDRICAL_SURFACE('',#9401,0.12645);
#8297=CYLINDRICAL_SURFACE('',#9402,0.12645);
#8298=CYLINDRICAL_SURFACE('',#9403,0.12645);
#8299=CYLINDRICAL_SURFACE('',#9405,0.1543);
#8300=CYLINDRICAL_SURFACE('',#9407,0.1543);
#8301=CYLINDRICAL_SURFACE('',#9408,0.1543);
#8302=CYLINDRICAL_SURFACE('',#9409,0.1543);
#8303=CYLINDRICAL_SURFACE('',#9410,0.1543);
#8304=CYLINDRICAL_SURFACE('',#9412,0.1543);
#8305=CYLINDRICAL_SURFACE('',#9414,0.12645);
#8741=ADVANCED_FACE('',(#1324),#8294,.F.);
#8742=ADVANCED_FACE('',(#1325),#8295,.F.);
#8743=ADVANCED_FACE('',(#1326),#8296,.F.);
#8744=ADVANCED_FACE('',(#1327),#8297,.F.);
#8745=ADVANCED_FACE('',(#1328),#8298,.F.);
#8746=ADVANCED_FACE('',(#1329),#8299,.F.);
#8747=ADVANCED_FACE('',(#1330),#8300,.F.);
#8748=ADVANCED_FACE('',(#1331),#8301,.F.);
#8749=ADVANCED_FACE('',(#1332),#8302,.F.);
#8750=ADVANCED_FACE('',(#1333),#8303,.F.);
#8751=ADVANCED_FACE('',(#1334),#8304,.F.);
#8752=ADVANCED_FACE('',(#1335),#158,.F.);
#8753=ADVANCED_FACE('',(#1336),#159,.F.);
#8754=ADVANCED_FACE('',(#1337,#635),#881,.T.);
#8755=ADVANCED_FACE('',(#1338),#8305,.F.);
#8756=ADVANCED_FACE('',(#1339),#882,.T.);
#8757=ADVANCED_FACE('',(#1340),#883,.T.);
#8758=ADVANCED_FACE('',(#1341),#884,.T.);
#8759=ADVANCED_FACE('',(#1342),#885,.T.);
#8760=ADVANCED_FACE('',(#1343),#886,.T.);
#8761=ADVANCED_FACE('',(#1344),#887,.T.);
#8762=ADVANCED_FACE('',(#1345,#636),#888,.F.);
#8809=CLOSED_SHELL('',(#8741,#8742,#8743,#8744,#8745,#8746,#8747,#8748,
#8749,#8750,#8751,#8752,#8753,#8754,#8755,#8756,#8757,#8758,#8759,#8760,
#8761,#8762));
#9396=AXIS2_PLACEMENT_3D('',#20578,#11152,#11153);
#9397=AXIS2_PLACEMENT_3D('',#20579,#11154,#11155);
#9398=AXIS2_PLACEMENT_3D('',#20584,#11157,#11158);
#9399=AXIS2_PLACEMENT_3D('',#20592,#11159,#11160);
#9400=AXIS2_PLACEMENT_3D('',#20616,#11162,#11163);
#9401=AXIS2_PLACEMENT_3D('',#20639,#11164,#11165);
#9402=AXIS2_PLACEMENT_3D('',#20693,#11167,#11168);
#9403=AXIS2_PLACEMENT_3D('',#20741,#11170,#11171);
#9404=AXIS2_PLACEMENT_3D('',#20760,#11173,#11174);
#9405=AXIS2_PLACEMENT_3D('',#20780,#11175,#11176);
#9406=AXIS2_PLACEMENT_3D('',#20793,#11178,#11179);
#9407=AXIS2_PLACEMENT_3D('',#20801,#11180,#11181);
#9408=AXIS2_PLACEMENT_3D('',#20826,#11183,#11184);
#9409=AXIS2_PLACEMENT_3D('',#20851,#11186,#11187);
#9410=AXIS2_PLACEMENT_3D('',#20876,#11189,#11190);
#9411=AXIS2_PLACEMENT_3D('',#20887,#11192,#11193);
#9412=AXIS2_PLACEMENT_3D('',#20893,#11194,#11195);
#9413=AXIS2_PLACEMENT_3D('',#21449,#11196,#11197);
#9414=AXIS2_PLACEMENT_3D('',#21462,#11204,#11205);
#9415=AXIS2_PLACEMENT_3D('',#21463,#11206,#11207);
#9416=AXIS2_PLACEMENT_3D('',#21469,#11211,#11212);
#9417=AXIS2_PLACEMENT_3D('',#21473,#11215,#11216);
#9418=AXIS2_PLACEMENT_3D('',#21477,#11219,#11220);
#9419=AXIS2_PLACEMENT_3D('',#21481,#11223,#11224);
#9420=AXIS2_PLACEMENT_3D('',#21485,#11227,#11228);
#9421=AXIS2_PLACEMENT_3D('',#21487,#11230,#11231);
#11152=DIRECTION('axis',(0.,0.,1.));
#11153=DIRECTION('refdir',(1.,0.,0.));
#11154=DIRECTION('center_axis',(0.,0.,-1.));
#11155=DIRECTION('ref_axis',(1.,0.,0.));
#11156=DIRECTION('',(0.,0.,-1.));
#11157=DIRECTION('center_axis',(0.,0.,-1.));
#11158=DIRECTION('ref_axis',(1.,0.,0.));
#11159=DIRECTION('center_axis',(0.,0.,-1.));
#11160=DIRECTION('ref_axis',(1.,0.,0.));
#11161=DIRECTION('',(0.,0.,-1.));
#11162=DIRECTION('center_axis',(0.,0.,-1.));
#11163=DIRECTION('ref_axis',(1.,0.,0.));
#11164=DIRECTION('center_axis',(0.,0.,-1.));
#11165=DIRECTION('ref_axis',(1.,0.,0.));
#11166=DIRECTION('',(0.,0.,-1.));
#11167=DIRECTION('center_axis',(0.,0.,-1.));
#11168=DIRECTION('ref_axis',(1.,0.,0.));
#11169=DIRECTION('',(0.,0.,-1.));
#11170=DIRECTION('center_axis',(0.,0.,-1.));
#11171=DIRECTION('ref_axis',(0.937385399639056,-0.348293859468591,0.));
#11172=DIRECTION('',(0.,0.,-1.));
#11173=DIRECTION('center_axis',(0.,0.,-1.));
#11174=DIRECTION('ref_axis',(1.,0.,0.));
#11175=DIRECTION('center_axis',(0.,0.,-1.));
#11176=DIRECTION('ref_axis',(0.28361887368566,0.958937085782627,0.));
#11177=DIRECTION('',(1.22464679914735E-16,8.07419868282478E-31,-1.));
#11178=DIRECTION('center_axis',(0.,0.,1.));
#11179=DIRECTION('ref_axis',(1.,6.71554824363804E-15,0.));
#11180=DIRECTION('center_axis',(0.,0.,-1.));
#11181=DIRECTION('ref_axis',(1.,6.71554824363804E-15,0.));
#11182=DIRECTION('',(1.22464679914735E-16,8.07419868282478E-31,-1.));
#11183=DIRECTION('center_axis',(0.,0.,-1.));
#11184=DIRECTION('ref_axis',(1.,6.71554824363804E-15,0.));
#11185=DIRECTION('',(1.22464679914735E-16,8.07419868282478E-31,-1.));
#11186=DIRECTION('center_axis',(0.,0.,-1.));
#11187=DIRECTION('ref_axis',(1.,6.71554824363804E-15,0.));
#11188=DIRECTION('',(1.22464679914735E-16,8.07419868282478E-31,-1.));
#11189=DIRECTION('center_axis',(0.,0.,-1.));
#11190=DIRECTION('ref_axis',(-0.60895050335979,-0.793208222636313,0.));
#11191=DIRECTION('',(1.22464679914735E-16,8.07419868282478E-31,-1.));
#11192=DIRECTION('center_axis',(0.,0.,-1.));
#11193=DIRECTION('ref_axis',(1.,6.71554824363804E-15,0.));
#11194=DIRECTION('center_axis',(0.,0.,-1.));
#11195=DIRECTION('ref_axis',(1.,6.71554824363804E-15,0.));
#11196=DIRECTION('center_axis',(0.,0.,1.));
#11197=DIRECTION('ref_axis',(1.,0.,0.));
#11198=DIRECTION('',(0.5,0.866025403784439,0.));
#11199=DIRECTION('',(-0.5,0.866025403784439,0.));
#11200=DIRECTION('',(-1.,0.,0.));
#11201=DIRECTION('',(-0.5,-0.866025403784439,0.));
#11202=DIRECTION('',(0.5,-0.866025403784439,0.));
#11203=DIRECTION('',(1.,-3.49629579342466E-16,0.));
#11204=DIRECTION('center_axis',(0.,0.,-1.));
#11205=DIRECTION('ref_axis',(1.,0.,0.));
#11206=DIRECTION('center_axis',(-3.49629579342466E-16,-1.,0.));
#11207=DIRECTION('ref_axis',(1.,-3.49629579342466E-16,0.));
#11208=DIRECTION('',(1.,-3.49629579342466E-16,0.));
#11209=DIRECTION('',(0.,0.,1.));
#11210=DIRECTION('',(0.,0.,1.));
#11211=DIRECTION('center_axis',(-0.866025403784439,-0.5,0.));
#11212=DIRECTION('ref_axis',(0.5,-0.866025403784439,0.));
#11213=DIRECTION('',(0.5,-0.866025403784439,0.));
#11214=DIRECTION('',(0.,0.,1.));
#11215=DIRECTION('center_axis',(-0.866025403784439,0.5,0.));
#11216=DIRECTION('ref_axis',(-0.5,-0.866025403784439,0.));
#11217=DIRECTION('',(-0.5,-0.866025403784439,0.));
#11218=DIRECTION('',(0.,0.,1.));
#11219=DIRECTION('center_axis',(0.,1.,0.));
#11220=DIRECTION('ref_axis',(-1.,0.,0.));
#11221=DIRECTION('',(-1.,0.,0.));
#11222=DIRECTION('',(0.,0.,1.));
#11223=DIRECTION('center_axis',(0.866025403784439,0.5,0.));
#11224=DIRECTION('ref_axis',(-0.5,0.866025403784439,0.));
#11225=DIRECTION('',(-0.5,0.866025403784439,0.));
#11226=DIRECTION('',(0.,0.,1.));
#11227=DIRECTION('center_axis',(0.866025403784439,-0.5,0.));
#11228=DIRECTION('ref_axis',(0.5,0.866025403784439,0.));
#11229=DIRECTION('',(0.5,0.866025403784439,0.));
#11230=DIRECTION('center_axis',(0.,0.,1.));
#11231=DIRECTION('ref_axis',(1.,0.,0.));
#20578=CARTESIAN_POINT('',(0.,0.,0.));
#20579=CARTESIAN_POINT('Origin',(0.,0.,0.12));
#20580=CARTESIAN_POINT('',(-0.12639138516214,8.91322620741042E-5,0.00934196736194174));
#20581=CARTESIAN_POINT('',(-0.12645,1.54856587752183E-17,-5.55111512312578E-17));
#20582=CARTESIAN_POINT('',(-0.12645,1.54856587752183E-17,0.12));
#20583=CARTESIAN_POINT('',(-0.0488748409397564,0.116622692573588,0.));
#20584=CARTESIAN_POINT('Origin',(0.,0.,0.));
#20585=CARTESIAN_POINT('Ctrl Pts',(-0.0489111879062984,0.116810626195002,
1.20007714660797E-17));
#20586=CARTESIAN_POINT('Ctrl Pts',(-0.0838963038512042,0.101957324585112,
0.00240024091002088));
#20587=CARTESIAN_POINT('Ctrl Pts',(-0.11198221847721,0.0702793053867637,
0.00480048182004174));
#20588=CARTESIAN_POINT('Ctrl Pts',(-0.122072221370749,0.0336561163696377,
0.00720072273006261));
#20589=CARTESIAN_POINT('Ctrl Pts',(-0.125072637487486,0.022765653033531,
0.00791447094068899));
#20590=CARTESIAN_POINT('Ctrl Pts',(-0.126481745582665,0.0114379076904012,
0.00862821915131536));
#20591=CARTESIAN_POINT('Ctrl Pts',(-0.12639138516214,8.91322620741042E-5,
0.00934196736194174));
#20592=CARTESIAN_POINT('Origin',(0.,0.,0.12));
#20593=CARTESIAN_POINT('',(-0.126396145829628,-9.95859796292312E-5,0.0593419673619417));
#20594=CARTESIAN_POINT('',(-0.126575671592806,-7.20628672610732E-5,0.0456580326380584));
#20595=CARTESIAN_POINT('',(-0.12645,1.54856587752183E-17,0.12));
#20596=CARTESIAN_POINT('',(-0.10808967569503,-0.0656218295092665,0.));
#20597=CARTESIAN_POINT('Ctrl Pts',(-0.126575671592806,-7.20628672610732E-5,
0.0456580326380584));
#20598=CARTESIAN_POINT('Ctrl Pts',(-0.126327459688109,0.0361497101693465,
0.0433719816070355));
#20599=CARTESIAN_POINT('Ctrl Pts',(-0.109912066394173,0.0725710138228805,
0.0410859305760125));
#20600=CARTESIAN_POINT('Ctrl Pts',(-0.0824515099939393,0.0961223418729112,
0.0387998795449896));
#20601=CARTESIAN_POINT('Ctrl Pts',(-0.05137998778939,0.122770586059505,
0.036213220908657));
#20602=CARTESIAN_POINT('Ctrl Pts',(-0.00616751748104999,0.132941603485868,
0.0336265622723243));
#20603=CARTESIAN_POINT('Ctrl Pts',(0.0333172074018229,0.122176268745047,
0.0310399036359917));
#20604=CARTESIAN_POINT('Ctrl Pts',(0.0728019322846963,0.111410934004226,
0.028453244999659));
#20605=CARTESIAN_POINT('Ctrl Pts',(0.106558911742102,0.0797092470962188,
0.0258665863633264));
#20606=CARTESIAN_POINT('Ctrl Pts',(0.11981357554495,0.0409763259700822,
0.0232799277269937));
#20607=CARTESIAN_POINT('Ctrl Pts',(0.133068239347797,0.00224340484394604,
0.0206932690906611));
#20608=CARTESIAN_POINT('Ctrl Pts',(0.125820587496086,-0.0435207505003201,
0.0181066104543285));
#20609=CARTESIAN_POINT('Ctrl Pts',(0.101166903546451,-0.0762076816581678,
0.0155199518179958));
#20610=CARTESIAN_POINT('Ctrl Pts',(0.0765132195968157,-0.108894612816016,
0.0129332931816632));
#20611=CARTESIAN_POINT('Ctrl Pts',(0.0344535035492562,-0.128504319787445,
0.0103466345453306));
#20612=CARTESIAN_POINT('Ctrl Pts',(-0.00636464094143544,-0.126469737202777,
0.00775997590899791));
#20613=CARTESIAN_POINT('Ctrl Pts',(-0.0471827854321269,-0.124435154618108,
0.00517331727266527));
#20614=CARTESIAN_POINT('Ctrl Pts',(-0.0867593583659505,-0.100756282477341,
0.00258665863633259));
#20615=CARTESIAN_POINT('Ctrl Pts',(-0.108089675695031,-0.0656218295092657,
-5.55111512312578E-17));
#20616=CARTESIAN_POINT('Origin',(0.,0.,0.));
#20617=CARTESIAN_POINT('Ctrl Pts',(-0.12639138516214,8.91322620741042E-5,
0.00934196736194174));
#20618=CARTESIAN_POINT('Ctrl Pts',(-0.126154274972366,-0.0296906128949183,
0.011214877787648));
#20619=CARTESIAN_POINT('Ctrl Pts',(-0.115592373032178,-0.0596151635265703,
0.0130877882133543));
#20620=CARTESIAN_POINT('Ctrl Pts',(-0.0963650578556872,-0.0821635787359664,
0.0149606986390606));
#20621=CARTESIAN_POINT('Ctrl Pts',(-0.0698103971670931,-0.113304978845907,
0.0175473572753932));
#20622=CARTESIAN_POINT('Ctrl Pts',(-0.0267272342632827,-0.130377059081323,
0.0201340159117258));
#20623=CARTESIAN_POINT('Ctrl Pts',(0.0139574509341311,-0.125868770046104,
0.0227206745480584));
#20624=CARTESIAN_POINT('Ctrl Pts',(0.0546421361315456,-0.121360481010885,
0.0253073331843911));
#20625=CARTESIAN_POINT('Ctrl Pts',(0.0929283436225635,-0.0952718227050311,
0.0278939918207237));
#20626=CARTESIAN_POINT('Ctrl Pts',(0.112018291148455,-0.0590635258734944,
0.0304806504570564));
#20627=CARTESIAN_POINT('Ctrl Pts',(0.131108238674346,-0.0228552290419586,
0.033067309093389));
#20628=CARTESIAN_POINT('Ctrl Pts',(0.131001926235112,0.0234727063152593,
0.0356539677297216));
#20629=CARTESIAN_POINT('Ctrl Pts',(0.111741771403992,0.0595891814911641,
0.0382406263660542));
#20630=CARTESIAN_POINT('Ctrl Pts',(0.0924816165728724,0.0957056566670696,
0.0408272850023869));
#20631=CARTESIAN_POINT('Ctrl Pts',(0.0540676193498672,0.121610671661662,
0.0434139436387195));
#20632=CARTESIAN_POINT('Ctrl Pts',(0.0133639835211523,0.125930636937597,
0.0460006022750522));
#20633=CARTESIAN_POINT('Ctrl Pts',(-0.0273396523075625,0.130250602213533,
0.0485872609113848));
#20634=CARTESIAN_POINT('Ctrl Pts',(-0.0703329267419868,0.112985517770812,
0.0511739195477175));
#20635=CARTESIAN_POINT('Ctrl Pts',(-0.0967449447385466,0.0817152626609385,
0.0537605781840501));
#20636=CARTESIAN_POINT('Ctrl Pts',(-0.115741878896724,0.0592240248649833,
0.0556210412433473));
#20637=CARTESIAN_POINT('Ctrl Pts',(-0.126160906676814,0.0294875554882879,
0.0574815043026445));
#20638=CARTESIAN_POINT('Ctrl Pts',(-0.126396145829628,-9.95859796292312E-5,
0.0593419673619417));
#20639=CARTESIAN_POINT('Origin',(0.,0.,0.12));
#20640=CARTESIAN_POINT('',(-0.126529791093031,9.025049583615E-5,0.109341967361942));
#20641=CARTESIAN_POINT('',(-0.126349242904067,8.85860673823967E-5,0.0956580326380584));
#20642=CARTESIAN_POINT('',(-0.12645,1.54856587752183E-17,0.12));
#20643=CARTESIAN_POINT('Ctrl Pts',(-0.126349242904067,8.85860673823967E-5,
0.0956580326380584));
#20644=CARTESIAN_POINT('Ctrl Pts',(-0.126441591528965,0.0135570965972842,
0.0948119253946973));
#20645=CARTESIAN_POINT('Ctrl Pts',(-0.124448136217638,0.0269990101701626,
0.0939658181513361));
#20646=CARTESIAN_POINT('Ctrl Pts',(-0.120249444863787,0.0397126388809939,
0.093119710907975));
#20647=CARTESIAN_POINT('Ctrl Pts',(-0.107413505522824,0.0785798365820317,
0.0905330522716423));
#20648=CARTESIAN_POINT('Ctrl Pts',(-0.0739673525896496,0.110640458354997,
0.0879463936353097));
#20649=CARTESIAN_POINT('Ctrl Pts',(-0.0345920580258737,0.121821308595361,
0.085359734998977));
#20650=CARTESIAN_POINT('Ctrl Pts',(0.00478323653790218,0.133002158835724,
0.0827730763626444));
#20651=CARTESIAN_POINT('Ctrl Pts',(0.0500876727322792,0.123303237543486,
0.0801864177263117));
#20652=CARTESIAN_POINT('Ctrl Pts',(0.0814342209129887,0.0969820390626645,
0.077599759089979));
#20653=CARTESIAN_POINT('Ctrl Pts',(0.112780769093698,0.0706608405818426,
0.0750131004536464));
#20654=CARTESIAN_POINT('Ctrl Pts',(0.13016942926074,0.0277173649124373,
0.0724264418173139));
#20655=CARTESIAN_POINT('Ctrl Pts',(0.12596827751407,-0.0129984006283456,
0.0698397831809812));
#20656=CARTESIAN_POINT('Ctrl Pts',(0.121767125767399,-0.0537141661691284,
0.0672531245446486));
#20657=CARTESIAN_POINT('Ctrl Pts',(0.0959761621070158,-0.0922022215812886,
0.0646664659083159));
#20658=CARTESIAN_POINT('Ctrl Pts',(0.059914723710966,-0.111567668284471,
0.0620798072719833));
#20659=CARTESIAN_POINT('Ctrl Pts',(0.0238532853149157,-0.130933114987654,
0.0594931486356506));
#20660=CARTESIAN_POINT('Ctrl Pts',(-0.0224786278168013,-0.131175952981858,
0.056906489999318));
#20661=CARTESIAN_POINT('Ctrl Pts',(-0.0587401909579078,-0.112190380850839,
0.0543198313629853));
#20662=CARTESIAN_POINT('Ctrl Pts',(-0.0950017540990138,-0.0932048087198191,
0.0517331727266527));
#20663=CARTESIAN_POINT('Ctrl Pts',(-0.12119296724951,-0.0549908264635757,
0.0491465140903201));
#20664=CARTESIAN_POINT('Ctrl Pts',(-0.125823286774378,-0.0143210998620416,
0.0465598554539874));
#20665=CARTESIAN_POINT('Ctrl Pts',(-0.126361397696569,-0.0095946821776348,
0.0462592478486778));
#20666=CARTESIAN_POINT('Ctrl Pts',(-0.12660831057823,-0.00483509759607578,
0.0459586402433681));
#20667=CARTESIAN_POINT('Ctrl Pts',(-0.126575671592806,-7.20628672610732E-5,
0.0456580326380584));
#20668=CARTESIAN_POINT('Ctrl Pts',(-0.126396145829628,-9.95859796292312E-5,
0.0593419673619417));
#20669=CARTESIAN_POINT('Ctrl Pts',(-0.12648796685852,-0.0116483513064931,
0.0600681629389771));
#20670=CARTESIAN_POINT('Ctrl Pts',(-0.125028206814926,-0.0231743653405588,
0.0607943585160125));
#20671=CARTESIAN_POINT('Ctrl Pts',(-0.121921363946098,-0.034237873926493,
0.0615205540930479));
#20672=CARTESIAN_POINT('Ctrl Pts',(-0.110855003598394,-0.0736453296270277,
0.0641072127293806));
#20673=CARTESIAN_POINT('Ctrl Pts',(-0.0788915213442898,-0.107184815251071,
0.0666938713657133));
#20674=CARTESIAN_POINT('Ctrl Pts',(-0.0400617348236378,-0.120133683626334,
0.069280530002046));
#20675=CARTESIAN_POINT('Ctrl Pts',(-0.00123194830298627,-0.133082552001597,
0.0718671886383786));
#20676=CARTESIAN_POINT('Ctrl Pts',(0.0444641424842127,-0.125440803128081,
0.0744538472747112));
#20677=CARTESIAN_POINT('Ctrl Pts',(0.0769682295152699,-0.100563001286921,
0.0770405059110438));
#20678=CARTESIAN_POINT('Ctrl Pts',(0.109472316546327,-0.0756851994457607,
0.0796271645473764));
#20679=CARTESIAN_POINT('Ctrl Pts',(0.128784399821243,-0.0335713446369571,
0.0822138231837091));
#20680=CARTESIAN_POINT('Ctrl Pts',(0.126427276285523,0.00729262199647547,
0.0848004818200417));
#20681=CARTESIAN_POINT('Ctrl Pts',(0.124070152749803,0.0481565886299079,
0.0873871404563744));
#20682=CARTESIAN_POINT('Ctrl Pts',(0.100043822403448,0.0877706670879697,
0.0899737990927071));
#20683=CARTESIAN_POINT('Ctrl Pts',(0.0648947831756147,0.108746049780439,
0.0925604577290397));
#20684=CARTESIAN_POINT('Ctrl Pts',(0.0297457439477817,0.129721432472907,
0.0951471163653723));
#20685=CARTESIAN_POINT('Ctrl Pts',(-0.0165260041615291,0.132058119399784,
0.0977337750017049));
#20686=CARTESIAN_POINT('Ctrl Pts',(-0.0536093211433369,0.114730442741844,
0.100320433638038));
#20687=CARTESIAN_POINT('Ctrl Pts',(-0.0906926381251451,0.0974027660839045,
0.10290709227437));
#20688=CARTESIAN_POINT('Ctrl Pts',(-0.11858752397945,0.0604107258411485,
0.105493750910703));
#20689=CARTESIAN_POINT('Ctrl Pts',(-0.12504939731921,0.0199921027543164,
0.108080409547035));
#20690=CARTESIAN_POINT('Ctrl Pts',(-0.126099919499473,0.0134211506765118,
0.108500928818671));
#20691=CARTESIAN_POINT('Ctrl Pts',(-0.126583971845017,0.00675963476331471,
0.108921448090306));
#20692=CARTESIAN_POINT('Ctrl Pts',(-0.126529791093031,9.025049583615E-5,
0.109341967361942));
#20693=CARTESIAN_POINT('Origin',(0.,0.,0.12));
#20694=CARTESIAN_POINT('',(-0.126296536029262,-6.10717992316628E-5,0.159341967361942));
#20695=CARTESIAN_POINT('',(-0.126453631260982,-0.000102348163238207,0.145658032638058));
#20696=CARTESIAN_POINT('',(-0.12645,1.54856587752183E-17,0.12));
#20697=CARTESIAN_POINT('Ctrl Pts',(-0.126453631260982,-0.000102348163238207,
0.145658032638058));
#20698=CARTESIAN_POINT('Ctrl Pts',(-0.126183364177612,0.031552920325249,
0.143665210546026));
#20699=CARTESIAN_POINT('Ctrl Pts',(-0.114073771100105,0.0633928690595716,
0.141672388453994));
#20700=CARTESIAN_POINT('Ctrl Pts',(-0.0925489356314354,0.0864391430514358,
0.139679566361962));
#20701=CARTESIAN_POINT('Ctrl Pts',(-0.0646099631645552,0.116352924063146,
0.13709290772563));
#20702=CARTESIAN_POINT('Ctrl Pts',(-0.0208084524006029,0.131451366650306,
0.134506249089297));
#20703=CARTESIAN_POINT('Ctrl Pts',(0.0196287675426836,0.125106932552633,
0.131919590452964));
#20704=CARTESIAN_POINT('Ctrl Pts',(0.0600659874859703,0.11876249845496,
0.129332931816632));
#20705=CARTESIAN_POINT('Ctrl Pts',(0.097138916608591,0.0909751876724545,
0.126746273180299));
#20706=CARTESIAN_POINT('Ctrl Pts',(0.114574233156503,0.0539423598350403,
0.124159614543967));
#20707=CARTESIAN_POINT('Ctrl Pts',(0.132009549704415,0.0169095319976262,
0.121572955907634));
#20708=CARTESIAN_POINT('Ctrl Pts',(0.129807253677619,-0.0293688128946969,
0.118986297271301));
#20709=CARTESIAN_POINT('Ctrl Pts',(0.108934072954415,-0.0645786240759305,
0.116399638634969));
#20710=CARTESIAN_POINT('Ctrl Pts',(0.0880608922312115,-0.099788435257164,
0.113812979998636));
#20711=CARTESIAN_POINT('Ctrl Pts',(0.0485168268116012,-0.123929712727308,
0.111226321362303));
#20712=CARTESIAN_POINT('Ctrl Pts',(0.00765986125275547,-0.126405537442516,
0.108639662725971));
#20713=CARTESIAN_POINT('Ctrl Pts',(-0.0331971043060904,-0.128881362157723,
0.106053004089638));
#20714=CARTESIAN_POINT('Ctrl Pts',(-0.0753669700041717,-0.109691734117994,
0.103466345453305));
#20715=CARTESIAN_POINT('Ctrl Pts',(-0.100339039978837,-0.0772600332835736,
0.100879686816973));
#20716=CARTESIAN_POINT('Ctrl Pts',(-0.117142637704978,-0.0554368822612891,
0.0991391354240014));
#20717=CARTESIAN_POINT('Ctrl Pts',(-0.126159269908366,-0.0276178718881664,
0.0973985840310299));
#20718=CARTESIAN_POINT('Ctrl Pts',(-0.126349242904067,8.85860673823967E-5,
0.0956580326380584));
#20719=CARTESIAN_POINT('Ctrl Pts',(-0.126529791093031,9.025049583615E-5,
0.109341967361942));
#20720=CARTESIAN_POINT('Ctrl Pts',(-0.126250700293628,-0.0342644551610371,
0.111508106726639));
#20721=CARTESIAN_POINT('Ctrl Pts',(-0.111690189779818,-0.0688279388928191,
0.113674246091336));
#20722=CARTESIAN_POINT('Ctrl Pts',(-0.0867076257192948,-0.092297473337895,
0.115840385456033));
#20723=CARTESIAN_POINT('Ctrl Pts',(-0.0568751199544048,-0.120323220412367,
0.118427044092366));
#20724=CARTESIAN_POINT('Ctrl Pts',(-0.0121812475994092,-0.132529508630403,
0.121013702728699));
#20725=CARTESIAN_POINT('Ctrl Pts',(0.0277554439013372,-0.123558363290506,
0.123600361365031));
#20726=CARTESIAN_POINT('Ctrl Pts',(0.0676921354020838,-0.114587217950609,
0.126187020001364));
#20727=CARTESIAN_POINT('Ctrl Pts',(0.102871646048582,-0.0844386390527785,
0.128773678637697));
#20728=CARTESIAN_POINT('Ctrl Pts',(0.117851793294146,-0.0463464242807743,
0.131360337274029));
#20729=CARTESIAN_POINT('Ctrl Pts',(0.13283194053971,-0.00825420950877041,
0.133946995910362));
#20730=CARTESIAN_POINT('Ctrl Pts',(0.127612724384341,0.0377816411374068,
0.136533654546694));
#20731=CARTESIAN_POINT('Ctrl Pts',(0.104485135941302,0.0715534408109559,
0.139120313183027));
#20732=CARTESIAN_POINT('Ctrl Pts',(0.0813575474982633,0.105325240484505,
0.14170697181936));
#20733=CARTESIAN_POINT('Ctrl Pts',(0.0403215867675544,0.126832989185426,
0.144293630455692));
#20734=CARTESIAN_POINT('Ctrl Pts',(-0.000609841963000384,0.126635909896556,
0.146880289092025));
#20735=CARTESIAN_POINT('Ctrl Pts',(-0.0415412706935549,0.126438830607686,
0.149466947728358));
#20736=CARTESIAN_POINT('Ctrl Pts',(-0.0823681674239554,0.104536923329025,
0.15205360636469));
#20737=CARTESIAN_POINT('Ctrl Pts',(-0.10516942503222,0.0705438627883669,
0.154640265001023));
#20738=CARTESIAN_POINT('Ctrl Pts',(-0.118984510025511,0.0499477610899654,
0.156207499121329));
#20739=CARTESIAN_POINT('Ctrl Pts',(-0.126182304652747,0.0249129445447297,
0.157774733241635));
#20740=CARTESIAN_POINT('Ctrl Pts',(-0.126296536029262,-6.10717992316628E-5,
0.159341967361942));
#20741=CARTESIAN_POINT('Origin',(0.,0.,0.12));
#20742=CARTESIAN_POINT('',(-0.126625441102054,2.7778768752873E-5,0.209341967361942));
#20743=CARTESIAN_POINT('',(-0.126471935391749,0.000101176582396995,0.195658032638058));
#20744=CARTESIAN_POINT('',(-0.12645,1.54856587752183E-17,0.12));
#20745=CARTESIAN_POINT('',(0.0958116152722397,0.0825211298936481,0.24));
#20746=CARTESIAN_POINT('Ctrl Pts',(-0.126625441102054,2.7778768752873E-5,
0.209341967361942));
#20747=CARTESIAN_POINT('Ctrl Pts',(-0.126482885932031,-0.0388928622545336,
0.21180133566563));
#20748=CARTESIAN_POINT('Ctrl Pts',(-0.107125339127294,-0.077921419747323,
0.214260703969318));
#20749=CARTESIAN_POINT('Ctrl Pts',(-0.0759952538809665,-0.101287130411732,
0.216720072273006));
#20750=CARTESIAN_POINT('Ctrl Pts',(-0.0432539585932993,-0.12586218783339,
0.219306730909339));
#20751=CARTESIAN_POINT('Ctrl Pts',(0.0025100419330305,-0.133111106253138,
0.221893389545672));
#20752=CARTESIAN_POINT('Ctrl Pts',(0.0412155518054008,-0.119764891216682,
0.224480048182004));
#20753=CARTESIAN_POINT('Ctrl Pts',(0.0799210616777711,-0.106418676180227,
0.227066706818337));
#20754=CARTESIAN_POINT('Ctrl Pts',(0.111568080896182,-0.072477327687567,
0.229653365454669));
#20755=CARTESIAN_POINT('Ctrl Pts',(0.122246574267713,-0.0330282462555153,
0.232240024091002));
#20756=CARTESIAN_POINT('Ctrl Pts',(0.132925067639245,0.00642083517653631,
0.234826682727335));
#20757=CARTESIAN_POINT('Ctrl Pts',(0.122635035163896,0.0513776495479799,
0.237413341363667));
#20758=CARTESIAN_POINT('Ctrl Pts',(0.0958116152722397,0.0825211298936481,
0.24));
#20759=CARTESIAN_POINT('',(-0.0959791030802601,0.0826138105732953,0.24));
#20760=CARTESIAN_POINT('Origin',(0.,0.,0.24));
#20761=CARTESIAN_POINT('Ctrl Pts',(-0.0959791030802601,0.0826138105732953,
0.24));
#20762=CARTESIAN_POINT('Ctrl Pts',(-0.0710417758635208,0.111296717646776,
0.237599759089979));
#20763=CARTESIAN_POINT('Ctrl Pts',(-0.0322351762885183,0.128218895525122,
0.235199518179958));
#20764=CARTESIAN_POINT('Ctrl Pts',(0.00571352152256588,0.126497857083363,
0.232799277269937));
#20765=CARTESIAN_POINT('Ctrl Pts',(0.0466095526337785,0.124643152028446,
0.230212618633605));
#20766=CARTESIAN_POINT('Ctrl Pts',(0.0865092470399708,0.101136876245298,
0.227625959997272));
#20767=CARTESIAN_POINT('Ctrl Pts',(0.107920636628548,0.0662586835305903,
0.225039301360939));
#20768=CARTESIAN_POINT('Ctrl Pts',(0.129332026217125,0.0313804908158828,
0.222452642724607));
#20769=CARTESIAN_POINT('Ctrl Pts',(0.132255110988087,-0.014869618830384,
0.219865984088274));
#20770=CARTESIAN_POINT('Ctrl Pts',(0.115395215428634,-0.0521699181865619,
0.217279325451942));
#20771=CARTESIAN_POINT('Ctrl Pts',(0.0985353198691812,-0.0894702175427398,
0.214692666815609));
#20772=CARTESIAN_POINT('Ctrl Pts',(0.0618924439793129,-0.117820706608829,
0.212106008179276));
#20773=CARTESIAN_POINT('Ctrl Pts',(0.0215571925812854,-0.12478734248304,
0.209519349542944));
#20774=CARTESIAN_POINT('Ctrl Pts',(-0.0187780588167422,-0.13175397835725,
0.206932690906611));
#20775=CARTESIAN_POINT('Ctrl Pts',(-0.0628056857229291,-0.117336761039583,
0.204346032270278));
#20776=CARTESIAN_POINT('Ctrl Pts',(-0.0912027768750998,-0.0878586653637446,
0.201759373633946));
#20777=CARTESIAN_POINT('Ctrl Pts',(-0.113530209130371,-0.0646812849521466,
0.199725593301983));
#20778=CARTESIAN_POINT('Ctrl Pts',(-0.126194825294183,-0.0321932513395888,
0.197691812970021));
#20779=CARTESIAN_POINT('Ctrl Pts',(-0.126471935391749,0.000101176582396995,
0.195658032638058));
#20780=CARTESIAN_POINT('Origin',(0.,0.,0.350421172358873));
#20781=CARTESIAN_POINT('',(-0.154453350152392,-8.79343647196378E-5,0.0295788276411275));
#20782=CARTESIAN_POINT('',(-0.15422847552802,0.000108763211052777,0.025421172358873));
#20783=CARTESIAN_POINT('',(-0.1543,-1.01731279388251E-15,0.350421172358873));
#20784=CARTESIAN_POINT('',(0.15408394018464,-0.00816268198427004,0.));
#20785=CARTESIAN_POINT('Ctrl Pts',(-0.15422847552802,0.000108763211052763,
0.025421172358873));
#20786=CARTESIAN_POINT('Ctrl Pts',(-0.154338737393477,0.0139570514561378,
0.0247074241482466));
#20787=CARTESIAN_POINT('Ctrl Pts',(-0.146387882101843,0.0778735560251454,
0.0214070173012875));
#20788=CARTESIAN_POINT('Ctrl Pts',(-0.0581466660421577,0.171532975008042,
0.0155199518179959));
#20789=CARTESIAN_POINT('Ctrl Pts',(0.109502662757235,0.144085240745689,
0.00775997590899784));
#20790=CARTESIAN_POINT('Ctrl Pts',(0.156737212705124,0.0419221657566679,
0.00258665863633264));
#20791=CARTESIAN_POINT('Ctrl Pts',(0.15408394018464,-0.00816268198427004,
0.));
#20792=CARTESIAN_POINT('',(0.129620323775263,-0.0841289546921688,3.62607491890453E-17));
#20793=CARTESIAN_POINT('Origin',(0.,0.,0.));
#20794=CARTESIAN_POINT('Ctrl Pts',(-0.154453350152392,-8.7934364719636E-5,
0.0295788276411275));
#20795=CARTESIAN_POINT('Ctrl Pts',(-0.154150470777978,0.0441115087317509,
0.0272927766101045));
#20796=CARTESIAN_POINT('Ctrl Pts',(-0.111454882743928,0.138841433785012,
0.0224200669427489));
#20797=CARTESIAN_POINT('Ctrl Pts',(0.0476444145610997,0.174632482457551,
0.0149606986390605));
#20798=CARTESIAN_POINT('Ctrl Pts',(0.168251138196633,0.0613688951001999,
0.0073871404563744));
#20799=CARTESIAN_POINT('Ctrl Pts',(0.154676764047789,-0.0451013867871701,
0.00240024091002087));
#20800=CARTESIAN_POINT('Ctrl Pts',(0.129620323775263,-0.0841289546921688,
1.57209315010398E-17));
#20801=CARTESIAN_POINT('Origin',(0.,0.,0.350421172358873));
#20802=CARTESIAN_POINT('',(-0.154177051641736,0.000108096719625833,0.0795788276411275));
#20803=CARTESIAN_POINT('',(-0.154234284709463,-0.000121519309271207,0.075421172358873));
#20804=CARTESIAN_POINT('',(-0.1543,-1.01731279388251E-15,0.350421172358873));
#20805=CARTESIAN_POINT('Ctrl Pts',(-0.154234284709463,-0.000121519309271208,
0.0754211723588731));
#20806=CARTESIAN_POINT('Ctrl Pts',(-0.153947235272697,0.0359820467524117,
0.0735607092995758));
#20807=CARTESIAN_POINT('Ctrl Pts',(-0.123557126730793,0.122717061869437,
0.0691135876039459));
#20808=CARTESIAN_POINT('Ctrl Pts',(0.0191012565771036,0.180005302104073,
0.0620798072719832));
#20809=CARTESIAN_POINT('Ctrl Pts',(0.159724738700703,0.0851738948996701,
0.0543198313629854));
#20810=CARTESIAN_POINT('Ctrl Pts',(0.160113920417758,-0.0844204212478698,
0.0465598554539874));
#20811=CARTESIAN_POINT('Ctrl Pts',(0.0199582426985643,-0.179924098035372,
0.0387998795449896));
#20812=CARTESIAN_POINT('Ctrl Pts',(-0.123251388539896,-0.123176028715441,
0.0317536518466181));
#20813=CARTESIAN_POINT('Ctrl Pts',(-0.153939142967466,-0.0362298265692857,
0.0272940827845792));
#20814=CARTESIAN_POINT('Ctrl Pts',(-0.15422847552802,0.000108763211052763,
0.025421172358873));
#20815=CARTESIAN_POINT('Ctrl Pts',(-0.154177051641736,0.000108096719625859,
0.0795788276411275));
#20816=CARTESIAN_POINT('Ctrl Pts',(-0.154289739603949,0.0165429814548096,
0.0787327203977663));
#20817=CARTESIAN_POINT('Ctrl Pts',(-0.144420757340354,0.0830897487115299,
0.0752999545180725));
#20818=CARTESIAN_POINT('Ctrl Pts',(-0.0494457976037486,0.174130301808973,
0.0692805300020459));
#20819=CARTESIAN_POINT('Ctrl Pts',(0.11640175885633,0.13862511662766,0.061520554093048));
#20820=CARTESIAN_POINT('Ctrl Pts',(0.18005704388064,-0.0185795878987759,
0.0537605781840501));
#20821=CARTESIAN_POINT('Ctrl Pts',(0.0856431484406112,-0.159474177462153,
0.0460006022750521));
#20822=CARTESIAN_POINT('Ctrl Pts',(-0.0839657292871194,-0.160363143120653,
0.0382406263660544));
#20823=CARTESIAN_POINT('Ctrl Pts',(-0.151599316432495,-0.0616831513139142,
0.0327667014880793));
#20824=CARTESIAN_POINT('Ctrl Pts',(-0.154493177716258,-0.00590000442131094,
0.0298794352464371));
#20825=CARTESIAN_POINT('Ctrl Pts',(-0.154453350152392,-8.7934364719636E-5,
0.0295788276411275));
#20826=CARTESIAN_POINT('Origin',(0.,0.,0.350421172358873));
#20827=CARTESIAN_POINT('',(-0.154304431028624,-0.000124889850439479,0.129578827641127));
#20828=CARTESIAN_POINT('',(-0.154397364694779,0.000110127730384366,0.125421172358873));
#20829=CARTESIAN_POINT('',(-0.1543,-1.01731279388251E-15,0.350421172358873));
#20830=CARTESIAN_POINT('Ctrl Pts',(-0.154397364694779,0.000110127730384357,
0.125421172358873));
#20831=CARTESIAN_POINT('Ctrl Pts',(-0.154463478494948,0.00824841157753406,
0.125000653087238));
#20832=CARTESIAN_POINT('Ctrl Pts',(-0.150239588102603,0.0663774823757793,
0.121993475179269));
#20833=CARTESIAN_POINT('Ctrl Pts',(-0.0766286530280003,0.163994611436961,
0.116399638634969));
#20834=CARTESIAN_POINT('Ctrl Pts',(0.0927599764682439,0.155440618724813,
0.108639662725971));
#20835=CARTESIAN_POINT('Ctrl Pts',(0.180714016146597,0.0104239566588842,
0.100879686816973));
#20836=CARTESIAN_POINT('Ctrl Pts',(0.11001758793024,-0.143743725357685,
0.093119710907975));
#20837=CARTESIAN_POINT('Ctrl Pts',(-0.0572637123892103,-0.171718146500831,
0.0853597349989769));
#20838=CARTESIAN_POINT('Ctrl Pts',(-0.146220320052713,-0.0783754111826042,
0.0794602221492764));
#20839=CARTESIAN_POINT('Ctrl Pts',(-0.154346328875204,-0.0142138442593302,
0.0761473679359084));
#20840=CARTESIAN_POINT('Ctrl Pts',(-0.154234284709463,-0.000121519309271208,
0.0754211723588731));
#20841=CARTESIAN_POINT('Ctrl Pts',(-0.154304431028624,-0.000124889850439474,
0.129578827641127));
#20842=CARTESIAN_POINT('Ctrl Pts',(-0.153974638929265,0.0385022981904757,
0.127586005549095));
#20843=CARTESIAN_POINT('Ctrl Pts',(-0.120018027207353,0.127784966030512,
0.123006524820731));
#20844=CARTESIAN_POINT('Ctrl Pts',(0.0280571680938306,0.178826694862324,
0.115840385456033));
#20845=CARTESIAN_POINT('Ctrl Pts',(0.163771354656592,0.0771047007047774,
0.108080409547035));
#20846=CARTESIAN_POINT('Ctrl Pts',(0.155709331479018,-0.0923080778690166,
0.100320433638038));
#20847=CARTESIAN_POINT('Ctrl Pts',(0.0109489686262093,-0.180682908560435,
0.0925604577290397));
#20848=CARTESIAN_POINT('Ctrl Pts',(-0.126591758993125,-0.118094248159534,
0.0856465890634029));
#20849=CARTESIAN_POINT('Ctrl Pts',(-0.153945238013925,-0.0337005743957639,
0.0813193790340989));
#20850=CARTESIAN_POINT('Ctrl Pts',(-0.154177051641736,0.000108096719625859,
0.0795788276411275));
#20851=CARTESIAN_POINT('Origin',(0.,0.,0.350421172358873));
#20852=CARTESIAN_POINT('',(-0.154326766555531,0.000123460234585843,0.179578827641127));
#20853=CARTESIAN_POINT('',(-0.154112736333057,-7.45225671948511E-5,0.175421172358873));
#20854=CARTESIAN_POINT('',(-0.1543,-1.01731279388251E-15,0.350421172358873));
#20855=CARTESIAN_POINT('Ctrl Pts',(-0.154112736333057,-7.45225671948471E-5,
0.175421172358873));
#20856=CARTESIAN_POINT('Ctrl Pts',(-0.153973346049181,0.0303998999070902,
0.173853938238567));
#20857=CARTESIAN_POINT('Ctrl Pts',(-0.130694151755309,0.111367805862998,
0.169700045481928));
#20858=CARTESIAN_POINT('Ctrl Pts',(-0.000871711368246156,0.181012066871201,
0.162959494088956));
#20859=CARTESIAN_POINT('Ctrl Pts',(0.149350085565286,0.102277888352765,
0.155199518179958));
#20860=CARTESIAN_POINT('Ctrl Pts',(0.168456255263351,-0.0662471829332422,
0.14743954227096));
#20861=CARTESIAN_POINT('Ctrl Pts',(0.0396733728729688,-0.17661315503135,
0.139679566361963));
#20862=CARTESIAN_POINT('Ctrl Pts',(-0.115072782317819,-0.134350623919955,
0.1323401097246));
#20863=CARTESIAN_POINT('Ctrl Pts',(-0.154056805498669,-0.041811035439686,
0.12758731172357));
#20864=CARTESIAN_POINT('Ctrl Pts',(-0.154397364694779,0.000110127730384357,
0.125421172358873));
#20865=CARTESIAN_POINT('Ctrl Pts',(-0.154326766555531,0.000123460234585825,
0.179578827641127));
#20866=CARTESIAN_POINT('Ctrl Pts',(-0.154418689716183,0.0108361910665024,
0.179025949336757));
#20867=CARTESIAN_POINT('Ctrl Pts',(-0.148597337680631,0.071569631208062,
0.175886412396054));
#20868=CARTESIAN_POINT('Ctrl Pts',(-0.0683530255288039,0.167611467503216,
0.170160216819019));
#20869=CARTESIAN_POINT('Ctrl Pts',(0.100397202365132,0.150621028353064,
0.162400240910021));
#20870=CARTESIAN_POINT('Ctrl Pts',(0.18100910679194,0.00139719974911195,
0.154640265001023));
#20871=CARTESIAN_POINT('Ctrl Pts',(0.102711092909207,-0.149052183789333,
0.146880289092025));
#20872=CARTESIAN_POINT('Ctrl Pts',(-0.0657574679958034,-0.168648048308422,
0.139120313183027));
#20873=CARTESIAN_POINT('Ctrl Pts',(-0.148058381688037,-0.0731761882111772,
0.133353159366061));
#20874=CARTESIAN_POINT('Ctrl Pts',(-0.154402705029802,-0.0116353181791797,
0.130172664185428));
#20875=CARTESIAN_POINT('Ctrl Pts',(-0.154304431028624,-0.000124889850439474,
0.129578827641127));
#20876=CARTESIAN_POINT('Origin',(0.,0.,0.350421172358873));
#20877=CARTESIAN_POINT('',(-0.154128406284035,-0.000157308197905263,0.229578827641128));
#20878=CARTESIAN_POINT('',(-0.154514081154978,3.38969080117728E-5,0.225421172358873));
#20879=CARTESIAN_POINT('',(-0.1543,-1.01731279388251E-15,0.350421172358873));
#20880=CARTESIAN_POINT('',(-0.0398513841857245,-0.149064942821851,0.24));
#20881=CARTESIAN_POINT('Ctrl Pts',(-0.0398513841857245,-0.149064942821851,
0.24));
#20882=CARTESIAN_POINT('Ctrl Pts',(-0.0883048112969314,-0.136111285829332,
0.237413341363667));
#20883=CARTESIAN_POINT('Ctrl Pts',(-0.143745772087175,-0.0847488633265083,
0.233939617244043));
#20884=CARTESIAN_POINT('Ctrl Pts',(-0.154234229255939,-0.017399338864059,
0.230465893124419));
#20885=CARTESIAN_POINT('Ctrl Pts',(-0.154128406284035,-0.00015730819790527,
0.229578827641128));
#20886=CARTESIAN_POINT('',(0.0399565498027962,-0.149273502906638,0.24));
#20887=CARTESIAN_POINT('Origin',(0.,0.,0.24));
#20888=CARTESIAN_POINT('Ctrl Pts',(0.0399565498027963,-0.149273502906638,
0.24));
#20889=CARTESIAN_POINT('Ctrl Pts',(-0.00490373130458673,-0.161043406468747,
0.237599759089979));
#20890=CARTESIAN_POINT('Ctrl Pts',(-0.107666111297752,-0.141562671532916,
0.23274014987627));
#20891=CARTESIAN_POINT('Ctrl Pts',(-0.154340128899266,-0.0474588267763927,
0.227880540662561));
#20892=CARTESIAN_POINT('Ctrl Pts',(-0.154514081154978,3.3896908011755E-5,
0.225421172358873));
#20893=CARTESIAN_POINT('Origin',(0.,0.,0.350421172358873));
#20894=CARTESIAN_POINT('Ctrl Pts',(-0.154514081154978,3.3896908011755E-5,
0.225421172358873));
#20895=CARTESIAN_POINT('Ctrl Pts',(-0.154523084458981,0.00249199339844659,
0.225293882026228));
#20896=CARTESIAN_POINT('Ctrl Pts',(-0.153375868586475,0.0548933889046004,
0.222579933057251));
#20897=CARTESIAN_POINT('Ctrl Pts',(-0.0942515706791253,0.154556313135293,
0.217279325451942));
#20898=CARTESIAN_POINT('Ctrl Pts',(0.0750450248431312,0.164716481511431,
0.209519349542944));
#20899=CARTESIAN_POINT('Ctrl Pts',(0.178461260043253,0.0303012077178856,
0.201759373633945));
#20900=CARTESIAN_POINT('Ctrl Pts',(0.125203781387627,-0.130731709675357,
0.193999397724948));
#20901=CARTESIAN_POINT('Ctrl Pts',(-0.0379704533096903,-0.17698585337688,
0.18623942181595));
#20902=CARTESIAN_POINT('Ctrl Pts',(-0.141587477595567,-0.0899051669249145,
0.180046680027258));
#20903=CARTESIAN_POINT('Ctrl Pts',(-0.154203404262525,-0.019896942829432,
0.176440596874899));
#20904=CARTESIAN_POINT('Ctrl Pts',(-0.154112736333057,-7.45225671948471E-5,
0.175421172358873));
#20905=CARTESIAN_POINT('Ctrl Pts',(-0.154128406284035,-0.00015730819790527,
0.229578827641128));
#20906=CARTESIAN_POINT('Ctrl Pts',(-0.153925652370292,0.0328779499839183,
0.227879234488086));
#20907=CARTESIAN_POINT('Ctrl Pts',(-0.127638532780061,0.116591914860373,
0.223592982698713));
#20908=CARTESIAN_POINT('Ctrl Pts',(0.00818767200092134,0.180778621679153,
0.216720072273006));
#20909=CARTESIAN_POINT('Ctrl Pts',(0.154249898498561,0.0947283641859207,
0.208960096364008));
#20910=CARTESIAN_POINT('Ctrl Pts',(0.164950538597243,-0.0745810526211722,
0.201200120455011));
#20911=CARTESIAN_POINT('Ctrl Pts',(0.0308106631569891,-0.178364693496558,
0.193440144546012));
#20912=CARTESIAN_POINT('Ctrl Pts',(-0.118879635670858,-0.129347344159377,
0.186233046941385));
#20913=CARTESIAN_POINT('Ctrl Pts',(-0.153988624301243,-0.0392836590090855,
0.18161260797309));
#20914=CARTESIAN_POINT('Ctrl Pts',(-0.154326766555531,0.000123460234585825,
0.179578827641127));
#20915=CARTESIAN_POINT('Ctrl Pts',(0.0958116152722397,0.0825211298936481,
0.24));
#20916=CARTESIAN_POINT('Ctrl Pts',(0.122635035163896,0.0513776495479799,
0.237413341363667));
#20917=CARTESIAN_POINT('Ctrl Pts',(0.143215100114593,-0.0385359791949074,
0.232240024091002));
#20918=CARTESIAN_POINT('Ctrl Pts',(0.0482740424593604,-0.140360024672886,
0.224480048182004));
#20919=CARTESIAN_POINT('Ctrl Pts',(-0.0890179591196291,-0.118613269413641,
0.216720072273006));
#20920=CARTESIAN_POINT('Ctrl Pts',(-0.148173729266643,0.00709031985706173,
0.208960096364008));
#20921=CARTESIAN_POINT('Ctrl Pts',(-0.0772398646297824,0.126660050524678,
0.20120012045501));
#20922=CARTESIAN_POINT('Ctrl Pts',(0.0614999571705377,0.134986384232796,
0.193440144546013));
#20923=CARTESIAN_POINT('Ctrl Pts',(0.146250332679645,0.0248320655601208,
0.185680168637014));
#20924=CARTESIAN_POINT('Ctrl Pts',(0.102605431992647,-0.107135610424167,
0.177920192728017));
#20925=CARTESIAN_POINT('Ctrl Pts',(-0.0311170694815965,-0.145041225920327,
0.170160216819019));
#20926=CARTESIAN_POINT('Ctrl Pts',(-0.137521919612742,-0.0556176253575994,
0.162400240910021));
#20927=CARTESIAN_POINT('Ctrl Pts',(-0.123195064154356,0.0826350160503635,
0.154640265001023));
#20928=CARTESIAN_POINT('Ctrl Pts',(-0.000714373963154436,0.148340737886347,
0.146880289092025));
#20929=CARTESIAN_POINT('Ctrl Pts',(0.122393508228972,0.0838174917835845,
0.139120313183027));
#20930=CARTESIAN_POINT('Ctrl Pts',(0.138051156695079,-0.0542900601549481,
0.131360337274029));
#20931=CARTESIAN_POINT('Ctrl Pts',(0.032512624755586,-0.14473579684844,
0.123600361365031));
#20932=CARTESIAN_POINT('Ctrl Pts',(-0.101568992309399,-0.108116932194331,
0.115840385456033));
#20933=CARTESIAN_POINT('Ctrl Pts',(-0.146482409833755,0.0234186855983926,
0.108080409547036));
#20934=CARTESIAN_POINT('Ctrl Pts',(-0.0627977522708403,0.13439480632666,
0.100320433638038));
#20935=CARTESIAN_POINT('Ctrl Pts',(0.076017492057093,0.127384745546031,
0.0925604577290397));
#20936=CARTESIAN_POINT('Ctrl Pts',(0.148096483096158,0.00854251017184644,
0.0848004818200417));
#20937=CARTESIAN_POINT('Ctrl Pts',(0.0901602332714121,-0.117799054254564,
0.0770405059110438));
#20938=CARTESIAN_POINT('Ctrl Pts',(-0.0469280390901857,-0.140724300875114,
0.069280530002046));
#20939=CARTESIAN_POINT('Ctrl Pts',(-0.142818485852497,-0.0401058440029853,
0.0615205540930479));
#20940=CARTESIAN_POINT('Ctrl Pts',(-0.113326201176411,0.0957204333280909,
0.0537605781840501));
#20941=CARTESIAN_POINT('Ctrl Pts',(0.0156536221268617,0.147515686656254,
0.0460006022750521));
#20942=CARTESIAN_POINT('Ctrl Pts',(0.130895613795878,0.0698006416724775,
0.0382406263660543));
#20943=CARTESIAN_POINT('Ctrl Pts',(0.13121455111358,-0.0691831643991777,
0.0304806504570563));
#20944=CARTESIAN_POINT('Ctrl Pts',(0.0163559286405278,-0.147449139316739,
0.0227206745480584));
#20945=CARTESIAN_POINT('Ctrl Pts',(-0.112893560070904,-0.0962328986104914,
0.0149606986390606));
#20946=CARTESIAN_POINT('Ctrl Pts',(-0.142972035491037,0.0393992613429074,
0.00720072273006258));
#20947=CARTESIAN_POINT('Ctrl Pts',(-0.0476516261894416,0.140572551456688,
-0.000559253178935252));
#20948=CARTESIAN_POINT('Ctrl Pts',(0.0897382482543901,0.118078928660352,
-0.00831922908793326));
#20949=CARTESIAN_POINT('Ctrl Pts',(0.128447313976429,0.0343555272840613,
-0.0134925463605985));
#20950=CARTESIAN_POINT('Ctrl Pts',(0.126272937371016,-0.00668937872268922,
-0.0160792049969311));
#20951=CARTESIAN_POINT('Ctrl Pts',(0.102845629995666,0.0885794229410663,
0.245359734998977));
#20952=CARTESIAN_POINT('Ctrl Pts',(0.13163829265517,0.0551495423644061,
0.242773076362644));
#20953=CARTESIAN_POINT('Ctrl Pts',(0.153729244145676,-0.0413651001137901,
0.237599759089979));
#20954=CARTESIAN_POINT('Ctrl Pts',(0.0518180837997932,-0.150664563191773,
0.229839783180981));
#20955=CARTESIAN_POINT('Ctrl Pts',(-0.0955532172229155,-0.127321268762976,
0.222079807271983));
#20956=CARTESIAN_POINT('Ctrl Pts',(-0.159051911315084,0.00761085605850937,
0.214319831362985));
#20957=CARTESIAN_POINT('Ctrl Pts',(-0.0829104333128967,0.135958804728216,
0.206559855453988));
#20958=CARTESIAN_POINT('Ctrl Pts',(0.0660149797280689,0.144896416659008,
0.19879987954499));
#20959=CARTESIAN_POINT('Ctrl Pts',(0.156987308467515,0.0266551129460425,
0.191039903635992));
#20960=CARTESIAN_POINT('Ctrl Pts',(0.110138215124307,-0.11500097684123,
0.183279927726994));
#20961=CARTESIAN_POINT('Ctrl Pts',(-0.0334015307576278,-0.155689435072511,
0.175519951817996));
#20962=CARTESIAN_POINT('Ctrl Pts',(-0.147618098500879,-0.0597007962188336,
0.167759975908998));
#20963=CARTESIAN_POINT('Ctrl Pts',(-0.13223943620312,0.0887016700559064,
0.16));
#20964=CARTESIAN_POINT('Ctrl Pts',(-0.000766819764851659,0.159231180881298,
0.152240024091002));
#20965=CARTESIAN_POINT('Ctrl Pts',(0.131379034007743,0.0899709573066447,
0.144480048182004));
#20966=CARTESIAN_POINT('Ctrl Pts',(0.14818618955117,-0.0582757677477129,
0.136720072273006));
#20967=CARTESIAN_POINT('Ctrl Pts',(0.0348995407947136,-0.15536158290941,
0.128960096364009));
#20968=CARTESIAN_POINT('Ctrl Pts',(-0.109025685167754,-0.116054342400242,
0.12120012045501));
#20969=CARTESIAN_POINT('Ctrl Pts',(-0.157236423577976,0.0251379696208395,
0.113440144546013));
#20970=CARTESIAN_POINT('Ctrl Pts',(-0.0674080525232269,0.144261408030094,
0.105680168637014));
#20971=CARTESIAN_POINT('Ctrl Pts',(0.0815983201941432,0.136736703272292,
0.0979201927280168));
#20972=CARTESIAN_POINT('Ctrl Pts',(0.158968994112971,0.00916965900085902,
0.0901602168190187));
#20973=CARTESIAN_POINT('Ctrl Pts',(0.0967793514910216,-0.126447277955604,
0.0824002409100209));
#20974=CARTESIAN_POINT('Ctrl Pts',(-0.0503732635231939,-0.151055582750353,
0.0746402650010229));
#20975=CARTESIAN_POINT('Ctrl Pts',(-0.15330351242688,-0.0430502166284845,
0.066880289092025));
#20976=CARTESIAN_POINT('Ctrl Pts',(-0.121646050135849,0.102747753924341,
0.0591203131830272));
#20977=CARTESIAN_POINT('Ctrl Pts',(0.0168028336102756,0.158345558472194,
0.0513603372740292));
#20978=CARTESIAN_POINT('Ctrl Pts',(0.140505322097486,0.074925059414875,
0.0436003613650313));
#20979=CARTESIAN_POINT('Ctrl Pts',(0.140847674214973,-0.0742622500154084,
0.0358403854560334));
#20980=CARTESIAN_POINT('Ctrl Pts',(0.0175566999932067,-0.158274125556283,
0.0280804095470355));
#20981=CARTESIAN_POINT('Ctrl Pts',(-0.121181646661057,-0.103297841872129,
0.0203204336380376));
#20982=CARTESIAN_POINT('Ctrl Pts',(-0.153468334920127,0.0422917601656304,
0.0125604577290396));
#20983=CARTESIAN_POINT('Ctrl Pts',(-0.0511499728070136,0.150892692640473,
0.00480048182004178));
#20984=CARTESIAN_POINT('Ctrl Pts',(0.0963263864220051,0.126747699355464,
-0.00295949408895622));
#20985=CARTESIAN_POINT('Ctrl Pts',(0.137877280219327,0.0368777401082635,
-0.00813281136162143));
#20986=CARTESIAN_POINT('Ctrl Pts',(0.135543271642224,-0.00718047980988283,
-0.0107194699979541));
#20987=CARTESIAN_POINT('Ctrl Pts',(0.109879644719093,0.0946377159884845,
0.250719469997954));
#20988=CARTESIAN_POINT('Ctrl Pts',(0.140641550146443,0.0589214351808321,
0.248132811361621));
#20989=CARTESIAN_POINT('Ctrl Pts',(0.164243388176759,-0.0441942210326729,
0.242959494088956));
#20990=CARTESIAN_POINT('Ctrl Pts',(0.055362125140226,-0.160969101710661,
0.235199518179958));
#20991=CARTESIAN_POINT('Ctrl Pts',(-0.102088475326202,-0.13602926811231,
0.227439542270961));
#20992=CARTESIAN_POINT('Ctrl Pts',(-0.169930093363525,0.00813139225995705,
0.219679566361962));
#20993=CARTESIAN_POINT('Ctrl Pts',(-0.0885810019960112,0.145257558931755,
0.211919590452965));
#20994=CARTESIAN_POINT('Ctrl Pts',(0.0705300022856002,0.154806449085219,
0.204159614543967));
#20995=CARTESIAN_POINT('Ctrl Pts',(0.167724284255384,0.0284781603319641,
0.196399638634969));
#20996=CARTESIAN_POINT('Ctrl Pts',(0.117670998255967,-0.122866343258294,
0.188639662725971));
#20997=CARTESIAN_POINT('Ctrl Pts',(-0.0356859920336591,-0.166337644224695,
0.180879686816973));
#20998=CARTESIAN_POINT('Ctrl Pts',(-0.157714277389017,-0.0637839670800676,
0.173119710907975));
#20999=CARTESIAN_POINT('Ctrl Pts',(-0.141283808251885,0.0947683240614489,
0.165359734998977));
#21000=CARTESIAN_POINT('Ctrl Pts',(-0.000819265566548849,0.17012162387625,
0.157599759089979));
#21001=CARTESIAN_POINT('Ctrl Pts',(0.140364559786514,0.0961244228297045,
0.149839783180981));
#21002=CARTESIAN_POINT('Ctrl Pts',(0.158321222407261,-0.0622614753404775,
0.142079807271983));
#21003=CARTESIAN_POINT('Ctrl Pts',(0.0372864568338413,-0.16598736897038,
0.134319831362986));
#21004=CARTESIAN_POINT('Ctrl Pts',(-0.116482378026109,-0.123991752606152,
0.126559855453987));
#21005=CARTESIAN_POINT('Ctrl Pts',(-0.167990437322196,0.0268572536432864,
0.11879987954499));
#21006=CARTESIAN_POINT('Ctrl Pts',(-0.0720183527756138,0.154128009733527,
0.111039903635992));
#21007=CARTESIAN_POINT('Ctrl Pts',(0.0871791483311938,0.146088660998552,
0.103279927726994));
#21008=CARTESIAN_POINT('Ctrl Pts',(0.169841505129784,0.00979680782987164,
0.0955199518179957));
#21009=CARTESIAN_POINT('Ctrl Pts',(0.103398469710631,-0.135095501656644,
0.0877599759089979));
#21010=CARTESIAN_POINT('Ctrl Pts',(-0.0538184879562023,-0.161386864625592,
0.08));
#21011=CARTESIAN_POINT('Ctrl Pts',(-0.163788539001263,-0.0459945892539838,
0.0722400240910021));
#21012=CARTESIAN_POINT('Ctrl Pts',(-0.129965899095288,0.10977507452059,
0.0644800481820042));
#21013=CARTESIAN_POINT('Ctrl Pts',(0.0179520450936897,0.169175430288133,
0.0567200722730062));
#21014=CARTESIAN_POINT('Ctrl Pts',(0.150115030399095,0.0800494771572726,
0.0489600963640084));
#21015=CARTESIAN_POINT('Ctrl Pts',(0.150480797316365,-0.0793413356316391,
0.0412001204550104));
#21016=CARTESIAN_POINT('Ctrl Pts',(0.0187574713458855,-0.169099111795828,
0.0334401445460125));
#21017=CARTESIAN_POINT('Ctrl Pts',(-0.129469733251211,-0.110362785133767,
0.0256801686370146));
#21018=CARTESIAN_POINT('Ctrl Pts',(-0.163964634349217,0.0451842589883535,
0.0179201927280167));
#21019=CARTESIAN_POINT('Ctrl Pts',(-0.0546483194245858,0.161212833824257,
0.0101602168190188));
#21020=CARTESIAN_POINT('Ctrl Pts',(0.10291452458962,0.135416470050577,0.00240024091002082));
#21021=CARTESIAN_POINT('Ctrl Pts',(0.147307246462226,0.0393999529324658,
-0.00277307636264439));
#21022=CARTESIAN_POINT('Ctrl Pts',(0.144813605913432,-0.00767158089707644,
-0.00535973499897704));
#21023=CARTESIAN_POINT('Ctrl Pts',(0.116913659442519,0.100696009035903,
0.256079204996931));
#21024=CARTESIAN_POINT('Ctrl Pts',(0.149644807637716,0.0626933279972582,
0.253492546360598));
#21025=CARTESIAN_POINT('Ctrl Pts',(0.174757532207842,-0.0470233419515556,
0.248319229087933));
#21026=CARTESIAN_POINT('Ctrl Pts',(0.0589061664806588,-0.171273640229548,
0.240559253178935));
#21027=CARTESIAN_POINT('Ctrl Pts',(-0.108623733429488,-0.144737267461644,
0.232799277269938));
#21028=CARTESIAN_POINT('Ctrl Pts',(-0.180808275411966,0.00865192846140473,
0.225039301360939));
#21029=CARTESIAN_POINT('Ctrl Pts',(-0.0942515706791253,0.154556313135293,
0.217279325451942));
#21030=CARTESIAN_POINT('Ctrl Pts',(0.0750450248431312,0.164716481511431,
0.209519349542944));
#21031=CARTESIAN_POINT('Ctrl Pts',(0.178461260043253,0.0303012077178856,
0.201759373633945));
#21032=CARTESIAN_POINT('Ctrl Pts',(0.125203781387627,-0.130731709675357,
0.193999397724948));
#21033=CARTESIAN_POINT('Ctrl Pts',(-0.0379704533096903,-0.17698585337688,
0.18623942181595));
#21034=CARTESIAN_POINT('Ctrl Pts',(-0.167810456277154,-0.0678671379413016,
0.178479445906952));
#21035=CARTESIAN_POINT('Ctrl Pts',(-0.150328180300649,0.100834978066992,
0.170719469997954));
#21036=CARTESIAN_POINT('Ctrl Pts',(-0.000871711368246156,0.181012066871201,
0.162959494088956));
#21037=CARTESIAN_POINT('Ctrl Pts',(0.149350085565286,0.102277888352765,
0.155199518179958));
#21038=CARTESIAN_POINT('Ctrl Pts',(0.168456255263351,-0.0662471829332422,
0.14743954227096));
#21039=CARTESIAN_POINT('Ctrl Pts',(0.0396733728729688,-0.17661315503135,
0.139679566361963));
#21040=CARTESIAN_POINT('Ctrl Pts',(-0.123939070884463,-0.131929162812062,
0.131919590452964));
#21041=CARTESIAN_POINT('Ctrl Pts',(-0.178744451066417,0.0285765376657333,
0.124159614543967));
#21042=CARTESIAN_POINT('Ctrl Pts',(-0.0766286530280003,0.163994611436961,
0.116399638634969));
#21043=CARTESIAN_POINT('Ctrl Pts',(0.0927599764682439,0.155440618724813,
0.108639662725971));
#21044=CARTESIAN_POINT('Ctrl Pts',(0.180714016146597,0.0104239566588842,
0.100879686816973));
#21045=CARTESIAN_POINT('Ctrl Pts',(0.11001758793024,-0.143743725357685,
0.093119710907975));
#21046=CARTESIAN_POINT('Ctrl Pts',(-0.0572637123892103,-0.171718146500831,
0.0853597349989769));
#21047=CARTESIAN_POINT('Ctrl Pts',(-0.174273565575645,-0.048938961879483,
0.0775997590899791));
#21048=CARTESIAN_POINT('Ctrl Pts',(-0.138285748054726,0.11680239511684,
0.0698397831809812));
#21049=CARTESIAN_POINT('Ctrl Pts',(0.0191012565771036,0.180005302104073,
0.0620798072719832));
#21050=CARTESIAN_POINT('Ctrl Pts',(0.159724738700703,0.0851738948996701,
0.0543198313629854));
#21051=CARTESIAN_POINT('Ctrl Pts',(0.160113920417758,-0.0844204212478698,
0.0465598554539874));
#21052=CARTESIAN_POINT('Ctrl Pts',(0.0199582426985643,-0.179924098035372,
0.0387998795449896));
#21053=CARTESIAN_POINT('Ctrl Pts',(-0.137757819841364,-0.117427728395404,
0.0310399036359917));
#21054=CARTESIAN_POINT('Ctrl Pts',(-0.174460933778308,0.0480767578110765,
0.0232799277269937));
#21055=CARTESIAN_POINT('Ctrl Pts',(-0.0581466660421577,0.171532975008042,
0.0155199518179959));
#21056=CARTESIAN_POINT('Ctrl Pts',(0.109502662757235,0.144085240745689,
0.00775997590899784));
#21057=CARTESIAN_POINT('Ctrl Pts',(0.156737212705124,0.0419221657566679,
0.00258665863633264));
#21058=CARTESIAN_POINT('Ctrl Pts',(0.15408394018464,-0.00816268198427004,
0.));
#21059=CARTESIAN_POINT('Ctrl Pts',(0.15408394018464,-0.00816268198427004,
0.));
#21060=CARTESIAN_POINT('Ctrl Pts',(0.153697863146473,0.00250812953454787,
1.45220469349306E-17));
#21061=CARTESIAN_POINT('Ctrl Pts',(0.152123106309386,0.0130673133993916,
-2.32988231788825E-17));
#21062=CARTESIAN_POINT('Ctrl Pts',(0.149466152202855,0.0233620190894148,
-6.07153216591882E-17));
#21063=CARTESIAN_POINT('Ctrl Pts',(0.14793019248835,0.0293132898222067,
-8.23454409684948E-17));
#21064=CARTESIAN_POINT('Ctrl Pts',(0.146031563681721,0.0351760135160456,
3.17823908273165E-17));
#21065=CARTESIAN_POINT('Ctrl Pts',(0.143784059453749,0.0409171473780902,
6.24500451351651E-17));
#21066=CARTESIAN_POINT('Ctrl Pts',(0.142595904075608,0.0439522291322952,
7.86626679846993E-17));
#21067=CARTESIAN_POINT('Ctrl Pts',(0.141309213132582,0.0469553015723855,
1.03399090950918E-16));
#21068=CARTESIAN_POINT('Ctrl Pts',(0.13992871365498,0.0499144025840292,
1.00613961606655E-16));
#21069=CARTESIAN_POINT('Ctrl Pts',(0.135493978469587,0.0594202586791481,
9.16669744478229E-17));
#21070=CARTESIAN_POINT('Ctrl Pts',(0.130119641392827,0.0684241765595774,
5.76730757846686E-17));
#21071=CARTESIAN_POINT('Ctrl Pts',(0.123887660540245,0.0767683201192124,
1.38777878078145E-16));
#21072=CARTESIAN_POINT('Ctrl Pts',(0.120656388342022,0.0810947453345699,
1.808305895663E-16));
#21073=CARTESIAN_POINT('Ctrl Pts',(0.117193874983239,0.0852432898306738,
1.062697842984E-16));
#21074=CARTESIAN_POINT('Ctrl Pts',(0.11350808038867,0.0891875047540603,
1.14491749414469E-16));
#21075=CARTESIAN_POINT('Ctrl Pts',(0.110158526423333,0.0927719043720516,
1.21963656801269E-16));
#21076=CARTESIAN_POINT('Ctrl Pts',(0.106618991420749,0.0961915975683434,
1.17223950247179E-16));
#21077=CARTESIAN_POINT('Ctrl Pts',(0.102922970874274,0.0994011657423757,
1.02348685082632E-16));
#21078=CARTESIAN_POINT('Ctrl Pts',(0.0973787571548163,0.104215676830788,
8.00350512245867E-17));
#21079=CARTESIAN_POINT('Ctrl Pts',(0.0914754811895955,0.108568278221023,
6.56075743842472E-17));
#21080=CARTESIAN_POINT('Ctrl Pts',(0.0852365492443714,0.11239450959967,
3.29597460435593E-17));
#21081=CARTESIAN_POINT('Ctrl Pts',(0.0787787796913796,0.116354950379705,
-7.26807264206779E-19));
#21082=CARTESIAN_POINT('Ctrl Pts',(0.0719608771003193,0.11975150351845,
7.81983513604452E-17));
#21083=CARTESIAN_POINT('Ctrl Pts',(0.0648645680501024,0.122569786811788,
1.05818132034585E-16));
#21084=CARTESIAN_POINT('Ctrl Pts',(0.0619760396963809,0.123716959397427,
1.17060669392563E-16));
#21085=CARTESIAN_POINT('Ctrl Pts',(0.0590419697559043,0.124767587801255,
-1.70921410850511E-17));
#21086=CARTESIAN_POINT('Ctrl Pts',(0.0560804949635964,0.12571697313192,
-8.67361737988404E-19));
#21087=CARTESIAN_POINT('Ctrl Pts',(0.0481895916857994,0.128246627558523,
4.23638569993146E-17));
#21088=CARTESIAN_POINT('Ctrl Pts',(0.040081547172159,0.13006877931966,2.48189907303608E-17));
#21089=CARTESIAN_POINT('Ctrl Pts',(0.0318655688619291,0.131172622122806,
0.));
#21090=CARTESIAN_POINT('Ctrl Pts',(0.0267717292715239,0.131856995664207,
-1.5387571972871E-17));
#21091=CARTESIAN_POINT('Ctrl Pts',(0.0216363184326117,0.132264755542675,
5.61228976213782E-17));
#21092=CARTESIAN_POINT('Ctrl Pts',(0.0164863123329273,0.132388468809724,
3.03576608295941E-17));
#21093=CARTESIAN_POINT('Ctrl Pts',(0.0120733572364389,0.13249447666326,
8.27985532573229E-18));
#21094=CARTESIAN_POINT('Ctrl Pts',(0.00764667637530932,0.132391154756805,
7.9933444120104E-17));
#21095=CARTESIAN_POINT('Ctrl Pts',(0.00324855819595315,0.132074892239241,
9.62771529167128E-17));
#21096=CARTESIAN_POINT('Ctrl Pts',(-0.00215998367955725,0.131685971569047,
1.16375665467493E-16));
#21097=CARTESIAN_POINT('Ctrl Pts',(-0.00753310453775717,0.130975837616781,
1.12286849362194E-16));
#21098=CARTESIAN_POINT('Ctrl Pts',(-0.0128378223015392,0.129936202211006,
1.27068494615301E-16));
#21099=CARTESIAN_POINT('Ctrl Pts',(-0.0180922709275414,0.128906418710228,
1.41710064449709E-16));
#21100=CARTESIAN_POINT('Ctrl Pts',(-0.023283936630727,0.12755123862641,
1.19281234835921E-16));
#21101=CARTESIAN_POINT('Ctrl Pts',(-0.028350637156304,0.125868914531291,
9.19403442267708E-17));
#21102=CARTESIAN_POINT('Ctrl Pts',(-0.0326437071621008,0.124443463179602,
6.87741127091605E-17));
#21103=CARTESIAN_POINT('Ctrl Pts',(-0.0368509055758185,0.122782751372096,
3.08039683582783E-17));
#21104=CARTESIAN_POINT('Ctrl Pts',(-0.0409513668396969,0.120880349084932,
-1.95156391047391E-18));
#21105=CARTESIAN_POINT('Ctrl Pts',(-0.0436523616789034,0.119627226953286,
-2.45035827619675E-17));
#21106=CARTESIAN_POINT('Ctrl Pts',(-0.0463070048384274,0.118269169850402,
-4.56986185075063E-18));
#21107=CARTESIAN_POINT('Ctrl Pts',(-0.0489111879062984,0.116810626195002,
-1.73472347597681E-18));
#21108=CARTESIAN_POINT('Ctrl Pts',(0.0958116152722397,0.0825211298936481,
0.24));
#21109=CARTESIAN_POINT('Ctrl Pts',(0.102494250906434,0.0762804363331629,
0.24));
#21110=CARTESIAN_POINT('Ctrl Pts',(0.108399952301676,0.0693089192431419,
0.24));
#21111=CARTESIAN_POINT('Ctrl Pts',(0.113520383394708,0.0617855200816623,
0.24));
#21112=CARTESIAN_POINT('Ctrl Pts',(0.11760088593285,0.0557900777417299,
0.24));
#21113=CARTESIAN_POINT('Ctrl Pts',(0.1211824537664,0.0494427873910869,0.24));
#21114=CARTESIAN_POINT('Ctrl Pts',(0.124247292533427,0.0428169095598754,
0.24));
#21115=CARTESIAN_POINT('Ctrl Pts',(0.125635784531567,0.0398151273949318,
0.24));
#21116=CARTESIAN_POINT('Ctrl Pts',(0.126914357096627,0.0367636074968772,
0.24));
#21117=CARTESIAN_POINT('Ctrl Pts',(0.128080244072735,0.0336751552254939,
0.24));
#21118=CARTESIAN_POINT('Ctrl Pts',(0.13155694143068,0.024465331227027,0.24));
#21119=CARTESIAN_POINT('Ctrl Pts',(0.134041462136676,0.0149150332268467,
0.24));
#21120=CARTESIAN_POINT('Ctrl Pts',(0.135496608205084,0.00520422800883078,
0.24));
#21121=CARTESIAN_POINT('Ctrl Pts',(0.136052940597398,0.00149158663520877,
0.24));
#21122=CARTESIAN_POINT('Ctrl Pts',(0.136458356591543,-0.00224482315054724,
0.24));
#21123=CARTESIAN_POINT('Ctrl Pts',(0.136708928272429,-0.00599574054845843,
0.24));
#21124=CARTESIAN_POINT('Ctrl Pts',(0.136894600108428,-0.00877514370161729,
0.24));
#21125=CARTESIAN_POINT('Ctrl Pts',(0.136994942037659,-0.0115613689854128,
0.24));
#21126=CARTESIAN_POINT('Ctrl Pts',(0.137008733057845,-0.0143405417274864,
0.24));
#21127=CARTESIAN_POINT('Ctrl Pts',(0.137045731231951,-0.0217964308202384,
0.24));
#21128=CARTESIAN_POINT('Ctrl Pts',(0.136462408227525,-0.0292204075226799,
0.24));
#21129=CARTESIAN_POINT('Ctrl Pts',(0.135240454646173,-0.0365388974416549,
0.24));
#21130=CARTESIAN_POINT('Ctrl Pts',(0.134058793448489,-0.0436160693529878,
0.24));
#21131=CARTESIAN_POINT('Ctrl Pts',(0.132280018312676,-0.050595007513092,
0.24));
#21132=CARTESIAN_POINT('Ctrl Pts',(0.129952822193542,-0.0574290655609092,
0.24));
#21133=CARTESIAN_POINT('Ctrl Pts',(0.128850070284018,-0.0606674134165377,
0.24));
#21134=CARTESIAN_POINT('Ctrl Pts',(0.127623182384127,-0.0638741644409745,
0.24));
#21135=CARTESIAN_POINT('Ctrl Pts',(0.126284110088584,-0.067028198101918,
0.24));
#21136=CARTESIAN_POINT('Ctrl Pts',(0.122654675969015,-0.0755769205431157,
0.24));
#21137=CARTESIAN_POINT('Ctrl Pts',(0.118195290975453,-0.0837663478860722,
0.24));
#21138=CARTESIAN_POINT('Ctrl Pts',(0.113014989178579,-0.0915013065162071,
0.24));
#21139=CARTESIAN_POINT('Ctrl Pts',(0.108985931714537,-0.0975172866704144,
0.24));
#21140=CARTESIAN_POINT('Ctrl Pts',(0.104519884911976,-0.103258562704539,
0.24));
#21141=CARTESIAN_POINT('Ctrl Pts',(0.0996546828651377,-0.108675969178894,
0.24));
#21142=CARTESIAN_POINT('Ctrl Pts',(0.0972822643803542,-0.11131765910988,
0.24));
#21143=CARTESIAN_POINT('Ctrl Pts',(0.09482095240722,-0.113875293456495,
0.24));
#21144=CARTESIAN_POINT('Ctrl Pts',(0.0922773332174137,-0.116342466058553,
0.24));
#21145=CARTESIAN_POINT('Ctrl Pts',(0.0868426048671788,-0.121613857680014,
0.24));
#21146=CARTESIAN_POINT('Ctrl Pts',(0.0810310485854155,-0.126474759557936,
0.24));
#21147=CARTESIAN_POINT('Ctrl Pts',(0.0748870600798396,-0.130870957562724,
0.24));
#21148=CARTESIAN_POINT('Ctrl Pts',(0.0715378781224404,-0.133267392228159,
0.24));
#21149=CARTESIAN_POINT('Ctrl Pts',(0.0680912231566627,-0.135524142754832,
0.24));
#21150=CARTESIAN_POINT('Ctrl Pts',(0.0645638484115253,-0.13762659390894,
0.24));
#21151=CARTESIAN_POINT('Ctrl Pts',(0.0598451535113139,-0.140439117742,0.24));
#21152=CARTESIAN_POINT('Ctrl Pts',(0.0549775790306604,-0.142978967531553,
0.24));
#21153=CARTESIAN_POINT('Ctrl Pts',(0.0499773507040556,-0.145225083935062,
0.24));
#21154=CARTESIAN_POINT('Ctrl Pts',(0.0466920976074369,-0.146700828718701,
0.24));
#21155=CARTESIAN_POINT('Ctrl Pts',(0.0433495270099635,-0.148049731670784,
0.24));
#21156=CARTESIAN_POINT('Ctrl Pts',(0.039956549802796,-0.149273502906639,
0.24));
#21157=CARTESIAN_POINT('Ctrl Pts',(-0.126296536029262,-6.10717992316628E-5,
0.159341967361942));
#21158=CARTESIAN_POINT('Ctrl Pts',(-0.12637083907321,-0.0163056929409037,
0.160361391877968));
#21159=CARTESIAN_POINT('Ctrl Pts',(-0.12344809088261,-0.0325245895549842,
0.161380816393994));
#21160=CARTESIAN_POINT('Ctrl Pts',(-0.117399968681154,-0.0474794518833934,
0.162400240910021));
#21161=CARTESIAN_POINT('Ctrl Pts',(-0.102053636235694,-0.0854254922118417,
0.164986899546353));
#21162=CARTESIAN_POINT('Ctrl Pts',(-0.0665853528586453,-0.115233359066084,
0.167573558182686));
#21163=CARTESIAN_POINT('Ctrl Pts',(-0.0265641275910804,-0.123819689910512,
0.170160216819019));
#21164=CARTESIAN_POINT('Ctrl Pts',(0.0134570976764845,-0.13240602075494,
0.172746875455351));
#21165=CARTESIAN_POINT('Ctrl Pts',(0.058031264834566,-0.119770815589554,
0.175333534091684));
#21166=CARTESIAN_POINT('Ctrl Pts',(0.0875924985281064,-0.0914586003428122,
0.177920192728017));
#21167=CARTESIAN_POINT('Ctrl Pts',(0.117153732221647,-0.0631463850960709,
0.180506851364349));
#21168=CARTESIAN_POINT('Ctrl Pts',(0.131702032450646,-0.0191571597679751,
0.183093510000682));
#21169=CARTESIAN_POINT('Ctrl Pts',(0.124851119980295,0.0211965060081854,
0.185680168637015));
#21170=CARTESIAN_POINT('Ctrl Pts',(0.118000207509943,0.0615501717843459,
0.188266827273347));
#21171=CARTESIAN_POINT('Ctrl Pts',(0.0897500823402403,0.0982682780085711,
0.19085348590968));
#21172=CARTESIAN_POINT('Ctrl Pts',(0.0525017161220023,0.115239608835997,
0.193440144546013));
#21173=CARTESIAN_POINT('Ctrl Pts',(0.0152533499037644,0.132210939663423,
0.196026803182345));
#21174=CARTESIAN_POINT('Ctrl Pts',(-0.030993257363009,0.129435495094051,
0.198613461818678));
#21175=CARTESIAN_POINT('Ctrl Pts',(-0.0659388717692058,0.108119484364762,
0.20120012045501));
#21176=CARTESIAN_POINT('Ctrl Pts',(-0.100884486175403,0.0868034736354726,
0.203786779091343));
#21177=CARTESIAN_POINT('Ctrl Pts',(-0.124529107721023,0.0469468967462671,
0.206373437727676));
#21178=CARTESIAN_POINT('Ctrl Pts',(-0.126492123469331,0.00606801008988057,
0.208960096364008));
#21179=CARTESIAN_POINT('Ctrl Pts',(-0.126588724127832,0.00405634646811867,
0.209087386696653));
#21180=CARTESIAN_POINT('Ctrl Pts',(-0.126632819376787,0.00204220716288977,
0.209214677029297));
#21181=CARTESIAN_POINT('Ctrl Pts',(-0.126625441102054,2.7778768752873E-5,
0.209341967361942));
#21182=CARTESIAN_POINT('Ctrl Pts',(-0.0398513841857245,-0.149064942821851,
0.24));
#21183=CARTESIAN_POINT('Ctrl Pts',(-0.0883048112969314,-0.136111285829332,
0.237413341363667));
#21184=CARTESIAN_POINT('Ctrl Pts',(-0.170871437255804,-0.0596187094618861,
0.232240024091002));
#21185=CARTESIAN_POINT('Ctrl Pts',(-0.145169204726118,0.108307533342445,
0.224480048182004));
#21186=CARTESIAN_POINT('Ctrl Pts',(0.00818767200092134,0.180778621679153,
0.216720072273006));
#21187=CARTESIAN_POINT('Ctrl Pts',(0.154249898498561,0.0947283641859207,
0.208960096364008));
#21188=CARTESIAN_POINT('Ctrl Pts',(0.164950538597243,-0.0745810526211722,
0.201200120455011));
#21189=CARTESIAN_POINT('Ctrl Pts',(0.0308106631569891,-0.178364693496558,
0.193440144546012));
#21190=CARTESIAN_POINT('Ctrl Pts',(-0.13036283225522,-0.125587074703769,
0.185680168637015));
#21191=CARTESIAN_POINT('Ctrl Pts',(-0.17709781441264,0.03745832727601,0.177920192728017));
#21192=CARTESIAN_POINT('Ctrl Pts',(-0.0683530255288039,0.167611467503216,
0.170160216819019));
#21193=CARTESIAN_POINT('Ctrl Pts',(0.100397202365132,0.150621028353064,
0.162400240910021));
#21194=CARTESIAN_POINT('Ctrl Pts',(0.18100910679194,0.00139719974911195,
0.154640265001023));
#21195=CARTESIAN_POINT('Ctrl Pts',(0.102711092909207,-0.149052183789333,
0.146880289092025));
#21196=CARTESIAN_POINT('Ctrl Pts',(-0.0657574679958034,-0.168648048308422,
0.139120313183027));
#21197=CARTESIAN_POINT('Ctrl Pts',(-0.176497206835689,-0.0401861834345609,
0.131360337274029));
#21198=CARTESIAN_POINT('Ctrl Pts',(-0.132288575936487,0.123555290563421,
0.123600361365031));
#21199=CARTESIAN_POINT('Ctrl Pts',(0.0280571680938306,0.178826694862324,
0.115840385456033));
#21200=CARTESIAN_POINT('Ctrl Pts',(0.163771354656592,0.0771047007047774,
0.108080409547035));
#21201=CARTESIAN_POINT('Ctrl Pts',(0.155709331479018,-0.0923080778690166,
0.100320433638038));
#21202=CARTESIAN_POINT('Ctrl Pts',(0.0109489686262093,-0.180682908560435,
0.0925604577290397));
#21203=CARTESIAN_POINT('Ctrl Pts',(-0.143423754439364,-0.110434756566834,
0.0848004818200417));
#21204=CARTESIAN_POINT('Ctrl Pts',(-0.17188331593326,0.0567648465404429,
0.0770405059110439));
#21205=CARTESIAN_POINT('Ctrl Pts',(-0.0494457976037486,0.174130301808973,
0.0692805300020459));
#21206=CARTESIAN_POINT('Ctrl Pts',(0.11640175885633,0.13862511662766,0.061520554093048));
#21207=CARTESIAN_POINT('Ctrl Pts',(0.18005704388064,-0.0185795878987759,
0.0537605781840501));
#21208=CARTESIAN_POINT('Ctrl Pts',(0.0856431484406112,-0.159474177462153,
0.0460006022750521));
#21209=CARTESIAN_POINT('Ctrl Pts',(-0.0839657292871194,-0.160363143120653,
0.0382406263660544));
#21210=CARTESIAN_POINT('Ctrl Pts',(-0.179844832231877,-0.0204718628801216,
0.0304806504570563));
#21211=CARTESIAN_POINT('Ctrl Pts',(-0.117866479118068,0.137399078213474,
0.0227206745480585));
#21212=CARTESIAN_POINT('Ctrl Pts',(0.0476444145610997,0.174632482457551,
0.0149606986390605));
#21213=CARTESIAN_POINT('Ctrl Pts',(0.171219786572432,0.0585809927800803,
0.00720072273006264));
#21214=CARTESIAN_POINT('Ctrl Pts',(0.144688050375066,-0.108949473877577,
-0.000559253178935319));
#21215=CARTESIAN_POINT('Ctrl Pts',(-0.0092814439579932,-0.180735423716049,
-0.00831922908793317));
#21216=CARTESIAN_POINT('Ctrl Pts',(-0.105867686800049,-0.122947365648507,
-0.0134925463605985));
#21217=CARTESIAN_POINT('Ctrl Pts',(-0.131895903200816,-0.0800747195988904,
-0.0160792049969312));
#21218=CARTESIAN_POINT('Ctrl Pts',(-0.0374537582415196,-0.140096572423086,
0.245359734998977));
#21219=CARTESIAN_POINT('Ctrl Pts',(-0.0829920245295529,-0.127922261611689,
0.242773076362644));
#21220=CARTESIAN_POINT('Ctrl Pts',(-0.160591096949962,-0.0560317985556137,
0.237599759089979));
#21221=CARTESIAN_POINT('Ctrl Pts',(-0.13643521822445,0.101791299158848,
0.229839783180981));
#21222=CARTESIAN_POINT('Ctrl Pts',(0.00769506740980954,0.1699022237233,
0.222079807271983));
#21223=CARTESIAN_POINT('Ctrl Pts',(0.144969579481095,0.0890291096113304,
0.214319831362985));
#21224=CARTESIAN_POINT('Ctrl Pts',(0.155026424317845,-0.0700939445729984,
0.206559855453987));
#21225=CARTESIAN_POINT('Ctrl Pts',(0.0289569648011409,-0.167633527556011,
0.19879987954499));
#21226=CARTESIAN_POINT('Ctrl Pts',(-0.122519659046519,-0.118031231043151,
0.191039903635991));
#21227=CARTESIAN_POINT('Ctrl Pts',(-0.166442869216287,0.0352046776440443,
0.183279927726994));
#21228=CARTESIAN_POINT('Ctrl Pts',(-0.064240621638164,0.157527260611955,
0.175519951817996));
#21229=CARTESIAN_POINT('Ctrl Pts',(0.0943568867767351,0.141559037340679,
0.167759975908998));
#21230=CARTESIAN_POINT('Ctrl Pts',(0.170118841887737,0.00131313836865665,
0.16));
#21231=CARTESIAN_POINT('Ctrl Pts',(0.0965315639882279,-0.140084581027326,
0.152240024091002));
#21232=CARTESIAN_POINT('Ctrl Pts',(-0.0618012237018238,-0.158501476380598,
0.144480048182004));
#21233=CARTESIAN_POINT('Ctrl Pts',(-0.165878396703103,-0.0377684145673052,
0.136720072273006));
#21234=CARTESIAN_POINT('Ctrl Pts',(-0.124329541933827,0.116121687534276,
0.128960096364008));
#21235=CARTESIAN_POINT('Ctrl Pts',(0.0263691315170036,0.168067732987372,
0.12120012045501));
#21236=CARTESIAN_POINT('Ctrl Pts',(0.153918185014798,0.0724657594331675,
0.113440144546012));
#21237=CARTESIAN_POINT('Ctrl Pts',(0.146341206869619,-0.0867544378416841,
0.105680168637015));
#21238=CARTESIAN_POINT('Ctrl Pts',(0.0102902328814698,-0.169812269106107,
0.0979201927280167));
#21239=CARTESIAN_POINT('Ctrl Pts',(-0.134794781526993,-0.103790539737311,
0.0901602168190187));
#21240=CARTESIAN_POINT('Ctrl Pts',(-0.161542096774173,0.0533496359633175,
0.0824002409100209));
#21241=CARTESIAN_POINT('Ctrl Pts',(-0.0464709316213242,0.163653894581969,
0.074640265001023));
#21242=CARTESIAN_POINT('Ctrl Pts',(0.109398542213106,0.130284849835523,
0.066880289092025));
#21243=CARTESIAN_POINT('Ctrl Pts',(0.16922405906302,-0.0174617621848401,
0.0591203131830272));
#21244=CARTESIAN_POINT('Ctrl Pts',(0.0804904984426183,-0.149879543972585,
0.0513603372740291));
#21245=CARTESIAN_POINT('Ctrl Pts',(-0.0789139998409189,-0.150715025739123,
0.0436003613650314));
#21246=CARTESIAN_POINT('Ctrl Pts',(-0.169024614954586,-0.0192401899891918,
0.0358403854560333));
#21247=CARTESIAN_POINT('Ctrl Pts',(-0.110775138777956,0.12913257502003,
0.0280804095470356));
#21248=CARTESIAN_POINT('Ctrl Pts',(0.0447779273164969,0.164125861942445,
0.0203204336380375));
#21249=CARTESIAN_POINT('Ctrl Pts',(0.16091848811479,0.0550565152494576,
0.0125604577290397));
#21250=CARTESIAN_POINT('Ctrl Pts',(0.135983012131502,-0.10239461786658,
0.00480048182004171));
#21251=CARTESIAN_POINT('Ctrl Pts',(-0.00872303347143,-0.169861624730324,
-0.00295949408895612));
#21252=CARTESIAN_POINT('Ctrl Pts',(-0.0994982439886826,-0.115550337924785,
-0.00813281136162148));
#21253=CARTESIAN_POINT('Ctrl Pts',(-0.123960494032221,-0.0752570895690155,
-0.0107194699979541));
#21254=CARTESIAN_POINT('Ctrl Pts',(-0.0350561322973148,-0.13112820202432,
0.250719469997954));
#21255=CARTESIAN_POINT('Ctrl Pts',(-0.0776792377621743,-0.119733237394047,
0.248132811361621));
#21256=CARTESIAN_POINT('Ctrl Pts',(-0.150310756644121,-0.0524448876493412,
0.242959494088956));
#21257=CARTESIAN_POINT('Ctrl Pts',(-0.127701231722781,0.0952750649752511,
0.235199518179958));
#21258=CARTESIAN_POINT('Ctrl Pts',(0.00720246281869772,0.159025825767447,
0.22743954227096));
#21259=CARTESIAN_POINT('Ctrl Pts',(0.135689260463629,0.08332985503674,0.219679566361962));
#21260=CARTESIAN_POINT('Ctrl Pts',(0.145102310038447,-0.0656068365248246,
0.211919590452964));
#21261=CARTESIAN_POINT('Ctrl Pts',(0.0271032664452926,-0.156902361615465,
0.204159614543967));
#21262=CARTESIAN_POINT('Ctrl Pts',(-0.114676485837817,-0.110475387382534,
0.196399638634969));
#21263=CARTESIAN_POINT('Ctrl Pts',(-0.155787924019933,0.0329510280120788,
0.188639662725971));
#21264=CARTESIAN_POINT('Ctrl Pts',(-0.0601282177475243,0.147443053720694,
0.180879686816973));
#21265=CARTESIAN_POINT('Ctrl Pts',(0.0883165711883383,0.132497046328295,
0.173119710907975));
#21266=CARTESIAN_POINT('Ctrl Pts',(0.159228576983534,0.00122907698820117,
0.165359734998977));
#21267=CARTESIAN_POINT('Ctrl Pts',(0.0903520350672485,-0.131116978265319,
0.157599759089979));
#21268=CARTESIAN_POINT('Ctrl Pts',(-0.0578449794078444,-0.148354904452775,
0.149839783180981));
#21269=CARTESIAN_POINT('Ctrl Pts',(-0.155259586570517,-0.0353506457000499,
0.142079807271983));
#21270=CARTESIAN_POINT('Ctrl Pts',(-0.116370507931168,0.108688084505131,
0.134319831362985));
#21271=CARTESIAN_POINT('Ctrl Pts',(0.0246810949401768,0.157308771112418,
0.126559855453988));
#21272=CARTESIAN_POINT('Ctrl Pts',(0.144065015373005,0.0678268181615582,
0.118799879544989));
#21273=CARTESIAN_POINT('Ctrl Pts',(0.13697308226022,-0.0812007978143519,
0.111039903635992));
#21274=CARTESIAN_POINT('Ctrl Pts',(0.00963149713673027,-0.15894162965178,
0.103279927726994));
#21275=CARTESIAN_POINT('Ctrl Pts',(-0.126165808614623,-0.0971463229077874,
0.0955199518179957));
#21276=CARTESIAN_POINT('Ctrl Pts',(-0.151200877615086,0.0499344253861922,
0.087759975908998));
#21277=CARTESIAN_POINT('Ctrl Pts',(-0.0434960656388994,0.153177487354966,
0.08));
#21278=CARTESIAN_POINT('Ctrl Pts',(0.102395325569881,0.121944583043386,
0.072240024091002));
#21279=CARTESIAN_POINT('Ctrl Pts',(0.158391074245402,-0.0163439364709043,
0.0644800481820042));
#21280=CARTESIAN_POINT('Ctrl Pts',(0.0753378484446251,-0.140284910483017,
0.0567200722730062));
#21281=CARTESIAN_POINT('Ctrl Pts',(-0.0738622703947183,-0.141066908357593,
0.0489600963640083));
#21282=CARTESIAN_POINT('Ctrl Pts',(-0.158204397677296,-0.018008517098262,
0.0412001204550104));
#21283=CARTESIAN_POINT('Ctrl Pts',(-0.103683798437843,0.120866071826586,
0.0334401445460125));
#21284=CARTESIAN_POINT('Ctrl Pts',(0.0419114400718942,0.153619241427338,
0.0256801686370146));
#21285=CARTESIAN_POINT('Ctrl Pts',(0.150617189657149,0.051532037718835,
0.0179201927280167));
#21286=CARTESIAN_POINT('Ctrl Pts',(0.127277973887939,-0.0958397618555833,
0.0101602168190187));
#21287=CARTESIAN_POINT('Ctrl Pts',(-0.00816462298486686,-0.1589878257446,
0.00240024091002091));
#21288=CARTESIAN_POINT('Ctrl Pts',(-0.0931288011773165,-0.108153310201063,
-0.00277307636264444));
#21289=CARTESIAN_POINT('Ctrl Pts',(-0.116025084863626,-0.0704394595391406,
-0.00535973499897709));
#21290=CARTESIAN_POINT('Ctrl Pts',(-0.0326585063531099,-0.122159831625555,
0.256079204996931));
#21291=CARTESIAN_POINT('Ctrl Pts',(-0.0723664509947957,-0.111544213176404,
0.253492546360598));
#21292=CARTESIAN_POINT('Ctrl Pts',(-0.140030416338279,-0.0488579767430688,
0.248319229087933));
#21293=CARTESIAN_POINT('Ctrl Pts',(-0.118967245221113,0.0887588307916541,
0.240559253178936));
#21294=CARTESIAN_POINT('Ctrl Pts',(0.00670985822758596,0.148149427811594,
0.232799277269937));
#21295=CARTESIAN_POINT('Ctrl Pts',(0.126408941446163,0.0776306004621497,
0.225039301360939));
#21296=CARTESIAN_POINT('Ctrl Pts',(0.13517819575905,-0.0611197284766509,
0.217279325451942));
#21297=CARTESIAN_POINT('Ctrl Pts',(0.0252495680894444,-0.146171195674918,
0.209519349542944));
#21298=CARTESIAN_POINT('Ctrl Pts',(-0.106833312629116,-0.102919543721916,
0.201759373633946));
#21299=CARTESIAN_POINT('Ctrl Pts',(-0.14513297882358,0.0306973783801131,
0.193999397724948));
#21300=CARTESIAN_POINT('Ctrl Pts',(-0.0560158138568844,0.137358846829434,
0.18623942181595));
#21301=CARTESIAN_POINT('Ctrl Pts',(0.0822762555999414,0.12343505531591,
0.178479445906952));
#21302=CARTESIAN_POINT('Ctrl Pts',(0.148338312079331,0.00114501560774606,
0.170719469997954));
#21303=CARTESIAN_POINT('Ctrl Pts',(0.0841725061462688,-0.122149375503312,
0.162959494088956));
#21304=CARTESIAN_POINT('Ctrl Pts',(-0.0538887351138648,-0.138208332524951,
0.155199518179959));
#21305=CARTESIAN_POINT('Ctrl Pts',(-0.144640776437932,-0.0329328768327946,
0.14743954227096));
#21306=CARTESIAN_POINT('Ctrl Pts',(-0.108411473928508,0.101254481475986,
0.139679566361963));
#21307=CARTESIAN_POINT('Ctrl Pts',(0.0229930583633497,0.146549809237466,
0.131919590452964));
#21308=CARTESIAN_POINT('Ctrl Pts',(0.134211845731212,0.0631878768899486,
0.124159614543967));
#21309=CARTESIAN_POINT('Ctrl Pts',(0.127604957650822,-0.0756471577870196,
0.116399638634969));
#21310=CARTESIAN_POINT('Ctrl Pts',(0.00897276139199077,-0.148070990197453,
0.108639662725971));
#21311=CARTESIAN_POINT('Ctrl Pts',(-0.117536835702253,-0.0905021060782641,
0.100879686816973));
#21312=CARTESIAN_POINT('Ctrl Pts',(-0.140859658455999,0.0465192148090667,
0.0931197109079749));
#21313=CARTESIAN_POINT('Ctrl Pts',(-0.0405211996564747,0.142701080127962,
0.0853597349989771));
#21314=CARTESIAN_POINT('Ctrl Pts',(0.0953921089266558,0.113604316251249,
0.077599759089979));
#21315=CARTESIAN_POINT('Ctrl Pts',(0.147558089427783,-0.0152261107569683,
0.0698397831809813));
#21316=CARTESIAN_POINT('Ctrl Pts',(0.070185198446632,-0.130690276993449,
0.0620798072719832));
#21317=CARTESIAN_POINT('Ctrl Pts',(-0.0688105409485176,-0.131418790976063,
0.0543198313629854));
#21318=CARTESIAN_POINT('Ctrl Pts',(-0.147384180400005,-0.0167768442073323,
0.0465598554539874));
#21319=CARTESIAN_POINT('Ctrl Pts',(-0.0965924580977301,0.112599568633142,
0.0387998795449896));
#21320=CARTESIAN_POINT('Ctrl Pts',(0.0390449528272914,0.143112620912232,
0.0310399036359916));
#21321=CARTESIAN_POINT('Ctrl Pts',(0.140315891199508,0.0480075601882123,
0.0232799277269937));
#21322=CARTESIAN_POINT('Ctrl Pts',(0.118572935644375,-0.0892849058445864,
0.0155199518179958));
#21323=CARTESIAN_POINT('Ctrl Pts',(-0.00760621249830358,-0.148114026758875,
0.00775997590899793));
#21324=CARTESIAN_POINT('Ctrl Pts',(-0.0867593583659504,-0.100756282477341,
0.00258665863633259));
#21325=CARTESIAN_POINT('Ctrl Pts',(-0.108089675695031,-0.0656218295092657,
-5.55111512312578E-17));
#21326=CARTESIAN_POINT('Ctrl Pts',(-0.108089675695031,-0.0656218295092657,
-5.55111512312578E-17));
#21327=CARTESIAN_POINT('Ctrl Pts',(-0.104219465379748,-0.0739058869203245,
-4.02841154597017E-17));
#21328=CARTESIAN_POINT('Ctrl Pts',(-0.0994141168358061,-0.0816768736924768,
-5.16144647363644E-17));
#21329=CARTESIAN_POINT('Ctrl Pts',(-0.0938412360364922,-0.088871564406415,
-3.81639164714898E-17));
#21330=CARTESIAN_POINT('Ctrl Pts',(-0.0894001862863345,-0.094605040600905,
-2.74451237748006E-17));
#21331=CARTESIAN_POINT('Ctrl Pts',(-0.0844703330957707,-0.0999727304469881,
3.12377098840079E-17));
#21332=CARTESIAN_POINT('Ctrl Pts',(-0.0791158513129458,-0.104935071387697,
-1.21430643318376E-17));
#21333=CARTESIAN_POINT('Ctrl Pts',(-0.0766900604813501,-0.107183206995485,
-3.17962611543325E-17));
#21334=CARTESIAN_POINT('Ctrl Pts',(-0.0741829996358932,-0.109342173006691,
4.83248416902999E-17));
#21335=CARTESIAN_POINT('Ctrl Pts',(-0.0716059924168524,-0.111405381598006,
5.3776427755281E-17));
#21336=CARTESIAN_POINT('Ctrl Pts',(-0.0639212992135713,-0.117557915794061,
7.00331794132204E-17));
#21337=CARTESIAN_POINT('Ctrl Pts',(-0.0556061968393146,-0.12287204611112,
-5.69073736333764E-18));
#21338=CARTESIAN_POINT('Ctrl Pts',(-0.0468203466856493,-0.127256781127915,
5.55111512312578E-17));
#21339=CARTESIAN_POINT('Ctrl Pts',(-0.0434613267337519,-0.12893315986732,
7.89099528597243E-17));
#21340=CARTESIAN_POINT('Ctrl Pts',(-0.0400330653128497,-0.130473352587733,
3.97002991909352E-17));
#21341=CARTESIAN_POINT('Ctrl Pts',(-0.0365431560942257,-0.131870761756357,
6.59194920871187E-17));
#21342=CARTESIAN_POINT('Ctrl Pts',(-0.0339571636773035,-0.13290622981212,
8.5347686277821E-17));
#21343=CARTESIAN_POINT('Ctrl Pts',(-0.0313383144727484,-0.133862652235137,
-2.74403076010104E-17));
#21344=CARTESIAN_POINT('Ctrl Pts',(-0.0286994266230122,-0.134734580282325,
-2.42861286636753E-17));
#21345=CARTESIAN_POINT('Ctrl Pts',(-0.0216199050576346,-0.137073760181214,
-1.58242011095522E-17));
#21346=CARTESIAN_POINT('Ctrl Pts',(-0.0143790427459088,-0.138813119073991,
5.80198461902811E-17));
#21347=CARTESIAN_POINT('Ctrl Pts',(-0.0070411538297537,-0.139912507657099,
6.93889390390723E-17));
#21348=CARTESIAN_POINT('Ctrl Pts',(5.47883476400097E-5,-0.140975646920361,
8.02325614020808E-17));
#21349=CARTESIAN_POINT('Ctrl Pts',(0.00724182591717642,-0.141440539972256,
1.32011341321413E-16));
#21350=CARTESIAN_POINT('Ctrl Pts',(0.0144605478337719,-0.141339082434075,
1.61329283265843E-16));
#21351=CARTESIAN_POINT('Ctrl Pts',(0.0178811722145177,-0.141291006315792,
1.75221724083914E-16));
#21352=CARTESIAN_POINT('Ctrl Pts',(0.021310106848269,-0.141115105569205,
1.85534911235541E-16));
#21353=CARTESIAN_POINT('Ctrl Pts',(0.0247235715439624,-0.140816220288761,
1.71737624121704E-16));
#21354=CARTESIAN_POINT('Ctrl Pts',(0.0339754553361668,-0.140006119078294,
1.34341339582434E-16));
#21355=CARTESIAN_POINT('Ctrl Pts',(0.0431421008898472,-0.138295657968001,
8.04496487960062E-17));
#21356=CARTESIAN_POINT('Ctrl Pts',(0.0520992976556894,-0.135759125106636,
3.20923843055709E-17));
#21357=CARTESIAN_POINT('Ctrl Pts',(0.0590658916121619,-0.13378629867842,
-5.518202506064E-18));
#21358=CARTESIAN_POINT('Ctrl Pts',(0.0659062642374416,-0.131312982137409,
7.87850579480063E-17));
#21359=CARTESIAN_POINT('Ctrl Pts',(0.0725619642951071,-0.128359965266718,
7.63278329429795E-17));
#21360=CARTESIAN_POINT('Ctrl Pts',(0.0758074813473741,-0.126919986522721,
7.51296170399226E-17));
#21361=CARTESIAN_POINT('Ctrl Pts',(0.0790005264283722,-0.125369490597537,
8.38688896655138E-17));
#21362=CARTESIAN_POINT('Ctrl Pts',(0.0821329715644795,-0.123712761836801,
7.24247051220317E-17));
#21363=CARTESIAN_POINT('Ctrl Pts',(0.0888257654942848,-0.120172989003949,
4.79730178566093E-17));
#21364=CARTESIAN_POINT('Ctrl Pts',(0.0952446087626691,-0.116147988031934,
8.96774285244103E-17));
#21365=CARTESIAN_POINT('Ctrl Pts',(0.101324221742587,-0.111663228753314,
8.28330459778925E-17));
#21366=CARTESIAN_POINT('Ctrl Pts',(0.104638321741973,-0.109218510516871,
7.91020571356516E-17));
#21367=CARTESIAN_POINT('Ctrl Pts',(0.107849695272814,-0.106637925639498,
3.17151869302413E-17));
#21368=CARTESIAN_POINT('Ctrl Pts',(0.110939265073957,-0.10393289123317,
1.53956708492942E-17));
#21369=CARTESIAN_POINT('Ctrl Pts',(0.115072333360666,-0.100314234708527,
-6.43574216607592E-18));
#21370=CARTESIAN_POINT('Ctrl Pts',(0.118992075260627,-0.0964697210975667,
5.54296751400654E-17));
#21371=CARTESIAN_POINT('Ctrl Pts',(0.122673447199167,-0.0924082746861152,
3.52365706057789E-17));
#21372=CARTESIAN_POINT('Ctrl Pts',(0.125092164655522,-0.0897398425098966,
2.31620156359627E-17));
#21373=CARTESIAN_POINT('Ctrl Pts',(0.127407959881093,-0.0869777021544565,
-4.01489640485901E-17));
#21374=CARTESIAN_POINT('Ctrl Pts',(0.129620323775263,-0.0841289546921697,
-3.98986399474666E-17));
#21375=CARTESIAN_POINT('Ctrl Pts',(-0.126471935391749,0.000101176582396995,
0.195658032638058));
#21376=CARTESIAN_POINT('Ctrl Pts',(-0.126547267107008,0.00888033934128026,
0.195105154333688));
#21377=CARTESIAN_POINT('Ctrl Pts',(-0.125707148272093,0.0176451944231377,
0.194552276029318));
#21378=CARTESIAN_POINT('Ctrl Pts',(-0.12389684029672,0.0262048027713284,
0.193999397724948));
#21379=CARTESIAN_POINT('Ctrl Pts',(-0.115427257168015,0.0662512011965534,
0.191412739088615));
#21380=CARTESIAN_POINT('Ctrl Pts',(-0.0857215355124495,0.101805024012994,
0.188826080452282));
#21381=CARTESIAN_POINT('Ctrl Pts',(-0.0478199964418627,0.117261303502293,
0.18623942181595));
#21382=CARTESIAN_POINT('Ctrl Pts',(-0.0099184573712758,0.132717582991593,
0.183652763179617));
#21383=CARTESIAN_POINT('Ctrl Pts',(0.0361788991143328,0.128076319153751,
0.181066104543285));
#21384=CARTESIAN_POINT('Ctrl Pts',(0.070237920103702,0.105374013950137,
0.178479445906952));
#21385=CARTESIAN_POINT('Ctrl Pts',(0.104296941093071,0.0826717087465222,
0.175892787270619));
#21386=CARTESIAN_POINT('Ctrl Pts',(0.126317626586201,0.0419083621771342,
0.173306128634287));
#21387=CARTESIAN_POINT('Ctrl Pts',(0.126633668343922,0.000977623707263797,
0.170719469997954));
#21388=CARTESIAN_POINT('Ctrl Pts',(0.126949710101644,-0.0399531147626067,
0.168132811361621));
#21389=CARTESIAN_POINT('Ctrl Pts',(0.105561108123956,-0.08105124513296,
0.165546152725289));
#21390=CARTESIAN_POINT('Ctrl Pts',(0.0718566002584231,-0.104276803155076,
0.162959494088956));
#21391=CARTESIAN_POINT('Ctrl Pts',(0.0381520923928904,-0.127502361177192,
0.160372835452623));
#21392=CARTESIAN_POINT('Ctrl Pts',(-0.00786832136048696,-0.132855346851071,
0.157786176816291));
#21393=CARTESIAN_POINT('Ctrl Pts',(-0.0460038684578537,-0.117985930405985,
0.155199518179958));
#21394=CARTESIAN_POINT('Ctrl Pts',(-0.0841394155552204,-0.103116513960899,
0.152612859543626));
#21395=CARTESIAN_POINT('Ctrl Pts',(-0.114390095996576,-0.0680246953968468,
0.150026200907293));
#21396=CARTESIAN_POINT('Ctrl Pts',(-0.12347721913235,-0.0281142263966907,
0.14743954227096));
#21397=CARTESIAN_POINT('Ctrl Pts',(-0.125563410841138,-0.018951712774069,
0.14684570572666));
#21398=CARTESIAN_POINT('Ctrl Pts',(-0.126534167537385,-0.00953522996602069,
0.146251869182359));
#21399=CARTESIAN_POINT('Ctrl Pts',(-0.126453631260982,-0.000102348163238207,
0.145658032638058));
#21400=CARTESIAN_POINT('Ctrl Pts',(-0.0398513841857245,-0.149064942821851,
0.24));
#21401=CARTESIAN_POINT('Ctrl Pts',(-0.0498806325786677,-0.145400296738327,
0.24));
#21402=CARTESIAN_POINT('Ctrl Pts',(-0.0594363948008725,-0.140639648297949,
0.24));
#21403=CARTESIAN_POINT('Ctrl Pts',(-0.0684062055177017,-0.134931499399492,
0.24));
#21404=CARTESIAN_POINT('Ctrl Pts',(-0.0735915624001909,-0.131631676235849,
0.24));
#21405=CARTESIAN_POINT('Ctrl Pts',(-0.0785806353345173,-0.128014298080738,
0.24));
#21406=CARTESIAN_POINT('Ctrl Pts',(-0.0833462611484583,-0.124102693747304,
0.24));
#21407=CARTESIAN_POINT('Ctrl Pts',(-0.0858656342542594,-0.122034803580736,
0.24));
#21408=CARTESIAN_POINT('Ctrl Pts',(-0.0883241156266364,-0.11988309220465,
0.24));
#21409=CARTESIAN_POINT('Ctrl Pts',(-0.0907117892851122,-0.117655751751618,
0.24));
#21410=CARTESIAN_POINT('Ctrl Pts',(-0.0983819858496404,-0.110500611839494,
0.24));
#21411=CARTESIAN_POINT('Ctrl Pts',(-0.105284458416918,-0.102606966330569,
0.24));
#21412=CARTESIAN_POINT('Ctrl Pts',(-0.111294422020379,-0.0941015332659665,
0.24));
#21413=CARTESIAN_POINT('Ctrl Pts',(-0.114410577497229,-0.0896914812962706,
0.24));
#21414=CARTESIAN_POINT('Ctrl Pts',(-0.117286101138547,-0.0851164738413172,
0.24));
#21415=CARTESIAN_POINT('Ctrl Pts',(-0.119898298320422,-0.0803922539627851,
0.24));
#21416=CARTESIAN_POINT('Ctrl Pts',(-0.1222721977331,-0.0760990011896685,
0.24));
#21417=CARTESIAN_POINT('Ctrl Pts',(-0.124430744329062,-0.0716759619599862,
0.24));
#21418=CARTESIAN_POINT('Ctrl Pts',(-0.126341093034125,-0.0671690272221462,
0.24));
#21419=CARTESIAN_POINT('Ctrl Pts',(-0.129206708925078,-0.060408406100978,
0.24));
#21420=CARTESIAN_POINT('Ctrl Pts',(-0.131522065955468,-0.0534490321795157,
0.24));
#21421=CARTESIAN_POINT('Ctrl Pts',(-0.133233091500091,-0.0463330844490581,
0.24));
#21422=CARTESIAN_POINT('Ctrl Pts',(-0.135004134506116,-0.0389675313754268,
0.24));
#21423=CARTESIAN_POINT('Ctrl Pts',(-0.136127599829873,-0.0314337185245799,
0.24));
#21424=CARTESIAN_POINT('Ctrl Pts',(-0.136615064298196,-0.0238138180582873,
0.24));
#21425=CARTESIAN_POINT('Ctrl Pts',(-0.136813484749433,-0.0207121682209076,
0.24));
#21426=CARTESIAN_POINT('Ctrl Pts',(-0.136906013213758,-0.0175970392000076,
0.24));
#21427=CARTESIAN_POINT('Ctrl Pts',(-0.136893785357156,-0.0144871321155608,
0.24));
#21428=CARTESIAN_POINT('Ctrl Pts',(-0.136861203984761,-0.00620072149302863,
0.24));
#21429=CARTESIAN_POINT('Ctrl Pts',(-0.136088646936857,0.00207357465703332,
0.24));
#21430=CARTESIAN_POINT('Ctrl Pts',(-0.134599584032292,0.0102285531249486,
0.24));
#21431=CARTESIAN_POINT('Ctrl Pts',(-0.133676409755049,0.0152843948425598,
0.24));
#21432=CARTESIAN_POINT('Ctrl Pts',(-0.132477333465274,0.0202942984003417,
0.24));
#21433=CARTESIAN_POINT('Ctrl Pts',(-0.131003622030167,0.0252303138624672,
0.24));
#21434=CARTESIAN_POINT('Ctrl Pts',(-0.129740734874544,0.029460199292259,
0.24));
#21435=CARTESIAN_POINT('Ctrl Pts',(-0.128274507607502,0.0336384499732856,
0.24));
#21436=CARTESIAN_POINT('Ctrl Pts',(-0.126614574688298,0.0377237273426867,
0.24));
#21437=CARTESIAN_POINT('Ctrl Pts',(-0.124573382985647,0.042747324485064,
0.24));
#21438=CARTESIAN_POINT('Ctrl Pts',(-0.122237651925267,0.0476379767326878,
0.24));
#21439=CARTESIAN_POINT('Ctrl Pts',(-0.119609691052418,0.0523617558795304,
0.24));
#21440=CARTESIAN_POINT('Ctrl Pts',(-0.117006563775536,0.0570408964535612,
0.24));
#21441=CARTESIAN_POINT('Ctrl Pts',(-0.114113358229268,0.0615597689541448,
0.24));
#21442=CARTESIAN_POINT('Ctrl Pts',(-0.110947628485839,0.0658586917144141,
0.24));
#21443=CARTESIAN_POINT('Ctrl Pts',(-0.108265305855902,0.0695011687224882,
0.24));
#21444=CARTESIAN_POINT('Ctrl Pts',(-0.105385772272888,0.0729892759232728,
0.24));
#21445=CARTESIAN_POINT('Ctrl Pts',(-0.102309360287629,0.0763011815833395,
0.24));
#21446=CARTESIAN_POINT('Ctrl Pts',(-0.100282916666232,0.0784827457339379,
0.24));
#21447=CARTESIAN_POINT('Ctrl Pts',(-0.0981709975111385,0.0805877996091198,
0.24));
#21448=CARTESIAN_POINT('Ctrl Pts',(-0.0959791030802606,0.0826138105732947,
0.24));
#21449=CARTESIAN_POINT('Origin',(0.,0.,0.24));
#21450=CARTESIAN_POINT('',(0.158771324027147,-0.275,0.24));
#21451=CARTESIAN_POINT('',(0.317542648054294,0.,0.24));
#21452=CARTESIAN_POINT('',(0.158771324027147,-0.275,0.24));
#21453=CARTESIAN_POINT('',(0.158771324027147,0.275,0.24));
#21454=CARTESIAN_POINT('',(0.317542648054294,0.,0.24));
#21455=CARTESIAN_POINT('',(-0.158771324027147,0.275,0.24));
#21456=CARTESIAN_POINT('',(0.158771324027147,0.275,0.24));
#21457=CARTESIAN_POINT('',(-0.317542648054294,5.55111512312578E-17,0.24));
#21458=CARTESIAN_POINT('',(-0.158771324027147,0.275,0.24));
#21459=CARTESIAN_POINT('',(-0.158771324027147,-0.275,0.24));
#21460=CARTESIAN_POINT('',(-0.317542648054294,3.88877587532466E-17,0.24));
#21461=CARTESIAN_POINT('',(-0.158771324027147,-0.275,0.24));
#21462=CARTESIAN_POINT('Origin',(0.,0.,0.12));
#21463=CARTESIAN_POINT('Origin',(-0.158771324027147,-0.275,0.));
#21464=CARTESIAN_POINT('',(-0.158771324027147,-0.275,0.));
#21465=CARTESIAN_POINT('',(0.158771324027147,-0.275,0.));
#21466=CARTESIAN_POINT('',(-0.158771324027147,-0.275,0.));
#21467=CARTESIAN_POINT('',(0.158771324027147,-0.275,0.));
#21468=CARTESIAN_POINT('',(-0.158771324027147,-0.275,0.));
#21469=CARTESIAN_POINT('Origin',(-0.317542648054294,3.88877587532466E-17,
0.));
#21470=CARTESIAN_POINT('',(-0.317542648054294,3.88877587532466E-17,0.));
#21471=CARTESIAN_POINT('',(-0.317542648054294,3.88877587532466E-17,0.));
#21472=CARTESIAN_POINT('',(-0.317542648054294,3.88877587532466E-17,0.));
#21473=CARTESIAN_POINT('Origin',(-0.158771324027147,0.275,0.));
#21474=CARTESIAN_POINT('',(-0.158771324027147,0.275,0.));
#21475=CARTESIAN_POINT('',(-0.158771324027147,0.275,0.));
#21476=CARTESIAN_POINT('',(-0.158771324027147,0.275,0.));
#21477=CARTESIAN_POINT('Origin',(0.158771324027147,0.275,0.));
#21478=CARTESIAN_POINT('',(0.158771324027147,0.275,0.));
#21479=CARTESIAN_POINT('',(0.158771324027147,0.275,0.));
#21480=CARTESIAN_POINT('',(0.158771324027147,0.275,0.));
#21481=CARTESIAN_POINT('Origin',(0.317542648054294,0.,0.));
#21482=CARTESIAN_POINT('',(0.317542648054294,0.,0.));
#21483=CARTESIAN_POINT('',(0.317542648054294,0.,0.));
#21484=CARTESIAN_POINT('',(0.317542648054294,0.,0.));
#21485=CARTESIAN_POINT('Origin',(0.158771324027147,-0.275,0.));
#21486=CARTESIAN_POINT('',(0.158771324027147,-0.275,0.));
#21487=CARTESIAN_POINT('Origin',(0.,0.,0.));
#22114=UNCERTAINTY_MEASURE_WITH_UNIT(LENGTH_MEASURE(0.001),#22130,
'DISTANCE_ACCURACY_VALUE',
'Maximum model space distance between geometric entities at asserted c
onnectivities');
#22117=UNCERTAINTY_MEASURE_WITH_UNIT(LENGTH_MEASURE(0.001),#22130,
'DISTANCE_ACCURACY_VALUE',
'Maximum model space distance between geometric entities at asserted c
onnectivities');
#22126=(
GEOMETRIC_REPRESENTATION_CONTEXT(3)
GLOBAL_UNCERTAINTY_ASSIGNED_CONTEXT((#22114))
GLOBAL_UNIT_ASSIGNED_CONTEXT((#22130,#22132,#22133))
REPRESENTATION_CONTEXT('','3D')
);
#22129=(
GEOMETRIC_REPRESENTATION_CONTEXT(3)
GLOBAL_UNCERTAINTY_ASSIGNED_CONTEXT((#22117))
GLOBAL_UNIT_ASSIGNED_CONTEXT((#22130,#22132,#22133))
REPRESENTATION_CONTEXT('','3D')
);
#22130=(
LENGTH_UNIT()
NAMED_UNIT(*)
SI_UNIT(.CENTI.,.METRE.)
);
#22132=(
NAMED_UNIT(*)
PLANE_ANGLE_UNIT()
SI_UNIT($,.RADIAN.)
);
#22133=(
NAMED_UNIT(*)
SI_UNIT($,.STERADIAN.)
SOLID_ANGLE_UNIT()
);
#22142=SHAPE_DEFINITION_REPRESENTATION(#22153,#22180);
#22153=PRODUCT_DEFINITION_SHAPE('',$,#22192);
#22180=SHAPE_REPRESENTATION('',(#9396),#22126);
#22183=PRODUCT_DEFINITION_CONTEXT('part definition',#22218,'design');
#22192=PRODUCT_DEFINITION('2026-11-10-05-10-49-241','Hex nut M3',#22203,
#22183);
#22203=PRODUCT_DEFINITION_FORMATION('',$,#22228);
#22218=APPLICATION_CONTEXT(
'Core Data for Automotive Mechanical Design Process');
#22219=PRODUCT_CONTEXT('part definition',#22218,'mechanical');
#22228=PRODUCT('2026-11-10-05-10-49-241','Hex nut M3',$,(#22219));
#22236=PRESENTATION_STYLE_ASSIGNMENT((#22244));
#22244=SURFACE_STYLE_USAGE(.BOTH.,#22252);
#22252=SURFACE_SIDE_STYLE('',(#22260));
#22260=SURFACE_STYLE_FILL_AREA(#22268);
#22268=FILL_AREA_STYLE('Fastener gray',(#22276));
#22276=FILL_AREA_STYLE_COLOUR('Fastener gray',#22284);
#22284=COLOUR_RGB('Fastener gray',0.607843137254902,0.643137254901961,0.698039215686274);
ENDSEC;
END-ISO-10303-21;
